ISO-10303-21;
HEADER;
/* Generated by software containing ST-Developer
 * from STEP Tools, Inc. (www.steptools.com) 
 */
/* OPTION: using custom renumber hook */

FILE_DESCRIPTION(
/* description */ ('STEP AP242 Edition 2', 'CAx-IF Rec.Pracs.---Representation and Presentation of Product Manufa
cturing Information (PMI)---4.0---2014-10-13', 'CAx-IF Rec.Pracs.---3D Tessellated Geometry---0.4---2014-09-14', '2;1', 'CAx-IF Rec.Pracs.---User Defined Attributes---1.5---2016-08-15'),
/* implementation_level */ '2;1');

FILE_NAME(
/* name */ 'spring.step',
/* time_stamp */ '2026-10-08T12:15:07Z',
/* author */ (''),
/* organization */ (''),
/* preprocessor_version */ 'ST-DEVELOPER v20',
/* originating_system */ 'ONSHAPE BY PTC INC, 1.221',
/* authorisation */ '  ');

FILE_SCHEMA (('AP242_MANAGED_MODEL_BASED_3D_ENGINEERING_MIM_LF { 1 0 10303 442 3 1 4 }'));
ENDSEC;

DATA;
#60=COLOUR_RGB('', 0.66274510, 0.83137255, 0.94901961);
#205=SHAPE_REPRESENTATION_RELATIONSHIP('','',#13779,#232);
#232=ADVANCED_BREP_SHAPE_REPRESENTATION('',(#13723),#45469);
#438=CIRCLE('',#14005,0.000595);
#439=CIRCLE('',#14007,0.000594999999999988);
#1240=PLANE('',#14004);
#1241=PLANE('',#14006);
#2416=ORIENTED_EDGE('',*,*,#5855,.F.);
#2417=ORIENTED_EDGE('',*,*,#5856,.T.);
#2418=ORIENTED_EDGE('',*,*,#5856,.F.);
#2419=ORIENTED_EDGE('',*,*,#5855,.T.);
#5855=EDGE_CURVE('',#7641,#7641,#438,.T.);
#5856=EDGE_CURVE('',#7642,#7642,#439,.T.);
#7641=VERTEX_POINT('',#28566);
#7642=VERTEX_POINT('',#28569);
#10641=EDGE_LOOP('',(#2416));
#10642=EDGE_LOOP('',(#2417));
#10643=EDGE_LOOP('',(#2418));
#10644=EDGE_LOOP('',(#2419));
#11756=FACE_BOUND('',#10641,.T.);
#11757=FACE_BOUND('',#10642,.T.);
#11758=FACE_BOUND('',#10643,.T.);
#11759=FACE_BOUND('',#10644,.T.);
#12674=(
BOUNDED_SURFACE()
B_SPLINE_SURFACE(3,3,((#28570,#28571,#28572,#28573,#28574,#28575,#28576,
#28577,#28578,#28579,#28580,#28581,#28582,#28583,#28584,#28585,#28586,#28587,
#28588,#28589,#28590,#28591,#28592,#28593,#28594,#28595,#28596,#28597,#28598,
#28599,#28600,#28601,#28602,#28603,#28604,#28605,#28606,#28607,#28608,#28609,
#28610,#28611,#28612,#28613,#28614,#28615,#28616,#28617,#28618,#28619,#28620,
#28621,#28622,#28623,#28624,#28625,#28626,#28627,#28628,#28629,#28630,#28631,
#28632,#28633,#28634,#28635,#28636,#28637,#28638,#28639,#28640,#28641,#28642,
#28643,#28644,#28645,#28646,#28647,#28648,#28649,#28650,#28651,#28652,#28653,
#28654,#28655,#28656,#28657,#28658,#28659,#28660,#28661,#28662,#28663,#28664,
#28665,#28666,#28667,#28668,#28669,#28670,#28671,#28672,#28673,#28674,#28675,
#28676,#28677,#28678,#28679,#28680,#28681,#28682,#28683,#28684,#28685,#28686,
#28687,#28688,#28689,#28690,#28691,#28692,#28693,#28694,#28695,#28696,#28697,
#28698,#28699,#28700,#28701,#28702,#28703,#28704,#28705,#28706,#28707,#28708,
#28709,#28710,#28711,#28712,#28713,#28714,#28715,#28716,#28717,#28718,#28719,
#28720,#28721,#28722,#28723,#28724,#28725,#28726,#28727,#28728,#28729,#28730,
#28731,#28732,#28733,#28734,#28735,#28736,#28737,#28738,#28739,#28740,#28741,
#28742,#28743,#28744,#28745,#28746,#28747,#28748,#28749,#28750,#28751,#28752,
#28753,#28754,#28755,#28756,#28757,#28758,#28759,#28760,#28761,#28762,#28763,
#28764,#28765,#28766,#28767,#28768,#28769,#28770,#28771,#28772,#28773,#28774,
#28775,#28776,#28777,#28778,#28779,#28780,#28781,#28782,#28783,#28784,#28785,
#28786,#28787,#28788,#28789,#28790,#28791,#28792,#28793,#28794,#28795,#28796,
#28797,#28798,#28799,#28800,#28801,#28802,#28803,#28804,#28805,#28806,#28807,
#28808,#28809,#28810,#28811,#28812,#28813,#28814,#28815,#28816,#28817,#28818,
#28819,#28820,#28821,#28822,#28823,#28824,#28825,#28826,#28827,#28828,#28829,
#28830,#28831,#28832,#28833,#28834,#28835,#28836,#28837,#28838,#28839,#28840,
#28841,#28842,#28843,#28844,#28845,#28846,#28847,#28848,#28849,#28850,#28851,
#28852,#28853,#28854,#28855,#28856,#28857,#28858,#28859,#28860,#28861,#28862,
#28863,#28864,#28865,#28866,#28867,#28868,#28869,#28870,#28871,#28872,#28873,
#28874,#28875,#28876,#28877,#28878,#28879),(#28880,#28881,#28882,#28883,
#28884,#28885,#28886,#28887,#28888,#28889,#28890,#28891,#28892,#28893,#28894,
#28895,#28896,#28897,#28898,#28899,#28900,#28901,#28902,#28903,#28904,#28905,
#28906,#28907,#28908,#28909,#28910,#28911,#28912,#28913,#28914,#28915,#28916,
#28917,#28918,#28919,#28920,#28921,#28922,#28923,#28924,#28925,#28926,#28927,
#28928,#28929,#28930,#28931,#28932,#28933,#28934,#28935,#28936,#28937,#28938,
#28939,#28940,#28941,#28942,#28943,#28944,#28945,#28946,#28947,#28948,#28949,
#28950,#28951,#28952,#28953,#28954,#28955,#28956,#28957,#28958,#28959,#28960,
#28961,#28962,#28963,#28964,#28965,#28966,#28967,#28968,#28969,#28970,#28971,
#28972,#28973,#28974,#28975,#28976,#28977,#28978,#28979,#28980,#28981,#28982,
#28983,#28984,#28985,#28986,#28987,#28988,#28989,#28990,#28991,#28992,#28993,
#28994,#28995,#28996,#28997,#28998,#28999,#29000,#29001,#29002,#29003,#29004,
#29005,#29006,#29007,#29008,#29009,#29010,#29011,#29012,#29013,#29014,#29015,
#29016,#29017,#29018,#29019,#29020,#29021,#29022,#29023,#29024,#29025,#29026,
#29027,#29028,#29029,#29030,#29031,#29032,#29033,#29034,#29035,#29036,#29037,
#29038,#29039,#29040,#29041,#29042,#29043,#29044,#29045,#29046,#29047,#29048,
#29049,#29050,#29051,#29052,#29053,#29054,#29055,#29056,#29057,#29058,#29059,
#29060,#29061,#29062,#29063,#29064,#29065,#29066,#29067,#29068,#29069,#29070,
#29071,#29072,#29073,#29074,#29075,#29076,#29077,#29078,#29079,#29080,#29081,
#29082,#29083,#29084,#29085,#29086,#29087,#29088,#29089,#29090,#29091,#29092,
#29093,#29094,#29095,#29096,#29097,#29098,#29099,#29100,#29101,#29102,#29103,
#29104,#29105,#29106,#29107,#29108,#29109,#29110,#29111,#29112,#29113,#29114,
#29115,#29116,#29117,#29118,#29119,#29120,#29121,#29122,#29123,#29124,#29125,
#29126,#29127,#29128,#29129,#29130,#29131,#29132,#29133,#29134,#29135,#29136,
#29137,#29138,#29139,#29140,#29141,#29142,#29143,#29144,#29145,#29146,#29147,
#29148,#29149,#29150,#29151,#29152,#29153,#29154,#29155,#29156,#29157,#29158,
#29159,#29160,#29161,#29162,#29163,#29164,#29165,#29166,#29167,#29168,#29169,
#29170,#29171,#29172,#29173,#29174,#29175,#29176,#29177,#29178,#29179,#29180,
#29181,#29182,#29183,#29184,#29185,#29186,#29187,#29188,#29189),(#29190,
#29191,#29192,#29193,#29194,#29195,#29196,#29197,#29198,#29199,#29200,#29201,
#29202,#29203,#29204,#29205,#29206,#29207,#29208,#29209,#29210,#29211,#29212,
#29213,#29214,#29215,#29216,#29217,#29218,#29219,#29220,#29221,#29222,#29223,
#29224,#29225,#29226,#29227,#29228,#29229,#29230,#29231,#29232,#29233,#29234,
#29235,#29236,#29237,#29238,#29239,#29240,#29241,#29242,#29243,#29244,#29245,
#29246,#29247,#29248,#29249,#29250,#29251,#29252,#29253,#29254,#29255,#29256,
#29257,#29258,#29259,#29260,#29261,#29262,#29263,#29264,#29265,#29266,#29267,
#29268,#29269,#29270,#29271,#29272,#29273,#29274,#29275,#29276,#29277,#29278,
#29279,#29280,#29281,#29282,#29283,#29284,#29285,#29286,#29287,#29288,#29289,
#29290,#29291,#29292,#29293,#29294,#29295,#29296,#29297,#29298,#29299,#29300,
#29301,#29302,#29303,#29304,#29305,#29306,#29307,#29308,#29309,#29310,#29311,
#29312,#29313,#29314,#29315,#29316,#29317,#29318,#29319,#29320,#29321,#29322,
#29323,#29324,#29325,#29326,#29327,#29328,#29329,#29330,#29331,#29332,#29333,
#29334,#29335,#29336,#29337,#29338,#29339,#29340,#29341,#29342,#29343,#29344,
#29345,#29346,#29347,#29348,#29349,#29350,#29351,#29352,#29353,#29354,#29355,
#29356,#29357,#29358,#29359,#29360,#29361,#29362,#29363,#29364,#29365,#29366,
#29367,#29368,#29369,#29370,#29371,#29372,#29373,#29374,#29375,#29376,#29377,
#29378,#29379,#29380,#29381,#29382,#29383,#29384,#29385,#29386,#29387,#29388,
#29389,#29390,#29391,#29392,#29393,#29394,#29395,#29396,#29397,#29398,#29399,
#29400,#29401,#29402,#29403,#29404,#29405,#29406,#29407,#29408,#29409,#29410,
#29411,#29412,#29413,#29414,#29415,#29416,#29417,#29418,#29419,#29420,#29421,
#29422,#29423,#29424,#29425,#29426,#29427,#29428,#29429,#29430,#29431,#29432,
#29433,#29434,#29435,#29436,#29437,#29438,#29439,#29440,#29441,#29442,#29443,
#29444,#29445,#29446,#29447,#29448,#29449,#29450,#29451,#29452,#29453,#29454,
#29455,#29456,#29457,#29458,#29459,#29460,#29461,#29462,#29463,#29464,#29465,
#29466,#29467,#29468,#29469,#29470,#29471,#29472,#29473,#29474,#29475,#29476,
#29477,#29478,#29479,#29480,#29481,#29482,#29483,#29484,#29485,#29486,#29487,
#29488,#29489,#29490,#29491,#29492,#29493,#29494,#29495,#29496,#29497,#29498,
#29499),(#29500,#29501,#29502,#29503,#29504,#29505,#29506,#29507,#29508,
#29509,#29510,#29511,#29512,#29513,#29514,#29515,#29516,#29517,#29518,#29519,
#29520,#29521,#29522,#29523,#29524,#29525,#29526,#29527,#29528,#29529,#29530,
#29531,#29532,#29533,#29534,#29535,#29536,#29537,#29538,#29539,#29540,#29541,
#29542,#29543,#29544,#29545,#29546,#29547,#29548,#29549,#29550,#29551,#29552,
#29553,#29554,#29555,#29556,#29557,#29558,#29559,#29560,#29561,#29562,#29563,
#29564,#29565,#29566,#29567,#29568,#29569,#29570,#29571,#29572,#29573,#29574,
#29575,#29576,#29577,#29578,#29579,#29580,#29581,#29582,#29583,#29584,#29585,
#29586,#29587,#29588,#29589,#29590,#29591,#29592,#29593,#29594,#29595,#29596,
#29597,#29598,#29599,#29600,#29601,#29602,#29603,#29604,#29605,#29606,#29607,
#29608,#29609,#29610,#29611,#29612,#29613,#29614,#29615,#29616,#29617,#29618,
#29619,#29620,#29621,#29622,#29623,#29624,#29625,#29626,#29627,#29628,#29629,
#29630,#29631,#29632,#29633,#29634,#29635,#29636,#29637,#29638,#29639,#29640,
#29641,#29642,#29643,#29644,#29645,#29646,#29647,#29648,#29649,#29650,#29651,
#29652,#29653,#29654,#29655,#29656,#29657,#29658,#29659,#29660,#29661,#29662,
#29663,#29664,#29665,#29666,#29667,#29668,#29669,#29670,#29671,#29672,#29673,
#29674,#29675,#29676,#29677,#29678,#29679,#29680,#29681,#29682,#29683,#29684,
#29685,#29686,#29687,#29688,#29689,#29690,#29691,#29692,#29693,#29694,#29695,
#29696,#29697,#29698,#29699,#29700,#29701,#29702,#29703,#29704,#29705,#29706,
#29707,#29708,#29709,#29710,#29711,#29712,#29713,#29714,#29715,#29716,#29717,
#29718,#29719,#29720,#29721,#29722,#29723,#29724,#29725,#29726,#29727,#29728,
#29729,#29730,#29731,#29732,#29733,#29734,#29735,#29736,#29737,#29738,#29739,
#29740,#29741,#29742,#29743,#29744,#29745,#29746,#29747,#29748,#29749,#29750,
#29751,#29752,#29753,#29754,#29755,#29756,#29757,#29758,#29759,#29760,#29761,
#29762,#29763,#29764,#29765,#29766,#29767,#29768,#29769,#29770,#29771,#29772,
#29773,#29774,#29775,#29776,#29777,#29778,#29779,#29780,#29781,#29782,#29783,
#29784,#29785,#29786,#29787,#29788,#29789,#29790,#29791,#29792,#29793,#29794,
#29795,#29796,#29797,#29798,#29799,#29800,#29801,#29802,#29803,#29804,#29805,
#29806,#29807,#29808,#29809),(#29810,#29811,#29812,#29813,#29814,#29815,
#29816,#29817,#29818,#29819,#29820,#29821,#29822,#29823,#29824,#29825,#29826,
#29827,#29828,#29829,#29830,#29831,#29832,#29833,#29834,#29835,#29836,#29837,
#29838,#29839,#29840,#29841,#29842,#29843,#29844,#29845,#29846,#29847,#29848,
#29849,#29850,#29851,#29852,#29853,#29854,#29855,#29856,#29857,#29858,#29859,
#29860,#29861,#29862,#29863,#29864,#29865,#29866,#29867,#29868,#29869,#29870,
#29871,#29872,#29873,#29874,#29875,#29876,#29877,#29878,#29879,#29880,#29881,
#29882,#29883,#29884,#29885,#29886,#29887,#29888,#29889,#29890,#29891,#29892,
#29893,#29894,#29895,#29896,#29897,#29898,#29899,#29900,#29901,#29902,#29903,
#29904,#29905,#29906,#29907,#29908,#29909,#29910,#29911,#29912,#29913,#29914,
#29915,#29916,#29917,#29918,#29919,#29920,#29921,#29922,#29923,#29924,#29925,
#29926,#29927,#29928,#29929,#29930,#29931,#29932,#29933,#29934,#29935,#29936,
#29937,#29938,#29939,#29940,#29941,#29942,#29943,#29944,#29945,#29946,#29947,
#29948,#29949,#29950,#29951,#29952,#29953,#29954,#29955,#29956,#29957,#29958,
#29959,#29960,#29961,#29962,#29963,#29964,#29965,#29966,#29967,#29968,#29969,
#29970,#29971,#29972,#29973,#29974,#29975,#29976,#29977,#29978,#29979,#29980,
#29981,#29982,#29983,#29984,#29985,#29986,#29987,#29988,#29989,#29990,#29991,
#29992,#29993,#29994,#29995,#29996,#29997,#29998,#29999,#30000,#30001,#30002,
#30003,#30004,#30005,#30006,#30007,#30008,#30009,#30010,#30011,#30012,#30013,
#30014,#30015,#30016,#30017,#30018,#30019,#30020,#30021,#30022,#30023,#30024,
#30025,#30026,#30027,#30028,#30029,#30030,#30031,#30032,#30033,#30034,#30035,
#30036,#30037,#30038,#30039,#30040,#30041,#30042,#30043,#30044,#30045,#30046,
#30047,#30048,#30049,#30050,#30051,#30052,#30053,#30054,#30055,#30056,#30057,
#30058,#30059,#30060,#30061,#30062,#30063,#30064,#30065,#30066,#30067,#30068,
#30069,#30070,#30071,#30072,#30073,#30074,#30075,#30076,#30077,#30078,#30079,
#30080,#30081,#30082,#30083,#30084,#30085,#30086,#30087,#30088,#30089,#30090,
#30091,#30092,#30093,#30094,#30095,#30096,#30097,#30098,#30099,#30100,#30101,
#30102,#30103,#30104,#30105,#30106,#30107,#30108,#30109,#30110,#30111,#30112,
#30113,#30114,#30115,#30116,#30117,#30118,#30119),(#30120,#30121,#30122,
#30123,#30124,#30125,#30126,#30127,#30128,#30129,#30130,#30131,#30132,#30133,
#30134,#30135,#30136,#30137,#30138,#30139,#30140,#30141,#30142,#30143,#30144,
#30145,#30146,#30147,#30148,#30149,#30150,#30151,#30152,#30153,#30154,#30155,
#30156,#30157,#30158,#30159,#30160,#30161,#30162,#30163,#30164,#30165,#30166,
#30167,#30168,#30169,#30170,#30171,#30172,#30173,#30174,#30175,#30176,#30177,
#30178,#30179,#30180,#30181,#30182,#30183,#30184,#30185,#30186,#30187,#30188,
#30189,#30190,#30191,#30192,#30193,#30194,#30195,#30196,#30197,#30198,#30199,
#30200,#30201,#30202,#30203,#30204,#30205,#30206,#30207,#30208,#30209,#30210,
#30211,#30212,#30213,#30214,#30215,#30216,#30217,#30218,#30219,#30220,#30221,
#30222,#30223,#30224,#30225,#30226,#30227,#30228,#30229,#30230,#30231,#30232,
#30233,#30234,#30235,#30236,#30237,#30238,#30239,#30240,#30241,#30242,#30243,
#30244,#30245,#30246,#30247,#30248,#30249,#30250,#30251,#30252,#30253,#30254,
#30255,#30256,#30257,#30258,#30259,#30260,#30261,#30262,#30263,#30264,#30265,
#30266,#30267,#30268,#30269,#30270,#30271,#30272,#30273,#30274,#30275,#30276,
#30277,#30278,#30279,#30280,#30281,#30282,#30283,#30284,#30285,#30286,#30287,
#30288,#30289,#30290,#30291,#30292,#30293,#30294,#30295,#30296,#30297,#30298,
#30299,#30300,#30301,#30302,#30303,#30304,#30305,#30306,#30307,#30308,#30309,
#30310,#30311,#30312,#30313,#30314,#30315,#30316,#30317,#30318,#30319,#30320,
#30321,#30322,#30323,#30324,#30325,#30326,#30327,#30328,#30329,#30330,#30331,
#30332,#30333,#30334,#30335,#30336,#30337,#30338,#30339,#30340,#30341,#30342,
#30343,#30344,#30345,#30346,#30347,#30348,#30349,#30350,#30351,#30352,#30353,
#30354,#30355,#30356,#30357,#30358,#30359,#30360,#30361,#30362,#30363,#30364,
#30365,#30366,#30367,#30368,#30369,#30370,#30371,#30372,#30373,#30374,#30375,
#30376,#30377,#30378,#30379,#30380,#30381,#30382,#30383,#30384,#30385,#30386,
#30387,#30388,#30389,#30390,#30391,#30392,#30393,#30394,#30395,#30396,#30397,
#30398,#30399,#30400,#30401,#30402,#30403,#30404,#30405,#30406,#30407,#30408,
#30409,#30410,#30411,#30412,#30413,#30414,#30415,#30416,#30417,#30418,#30419,
#30420,#30421,#30422,#30423,#30424,#30425,#30426,#30427,#30428,#30429),
(#30430,#30431,#30432,#30433,#30434,#30435,#30436,#30437,#30438,#30439,
#30440,#30441,#30442,#30443,#30444,#30445,#30446,#30447,#30448,#30449,#30450,
#30451,#30452,#30453,#30454,#30455,#30456,#30457,#30458,#30459,#30460,#30461,
#30462,#30463,#30464,#30465,#30466,#30467,#30468,#30469,#30470,#30471,#30472,
#30473,#30474,#30475,#30476,#30477,#30478,#30479,#30480,#30481,#30482,#30483,
#30484,#30485,#30486,#30487,#30488,#30489,#30490,#30491,#30492,#30493,#30494,
#30495,#30496,#30497,#30498,#30499,#30500,#30501,#30502,#30503,#30504,#30505,
#30506,#30507,#30508,#30509,#30510,#30511,#30512,#30513,#30514,#30515,#30516,
#30517,#30518,#30519,#30520,#30521,#30522,#30523,#30524,#30525,#30526,#30527,
#30528,#30529,#30530,#30531,#30532,#30533,#30534,#30535,#30536,#30537,#30538,
#30539,#30540,#30541,#30542,#30543,#30544,#30545,#30546,#30547,#30548,#30549,
#30550,#30551,#30552,#30553,#30554,#30555,#30556,#30557,#30558,#30559,#30560,
#30561,#30562,#30563,#30564,#30565,#30566,#30567,#30568,#30569,#30570,#30571,
#30572,#30573,#30574,#30575,#30576,#30577,#30578,#30579,#30580,#30581,#30582,
#30583,#30584,#30585,#30586,#30587,#30588,#30589,#30590,#30591,#30592,#30593,
#30594,#30595,#30596,#30597,#30598,#30599,#30600,#30601,#30602,#30603,#30604,
#30605,#30606,#30607,#30608,#30609,#30610,#30611,#30612,#30613,#30614,#30615,
#30616,#30617,#30618,#30619,#30620,#30621,#30622,#30623,#30624,#30625,#30626,
#30627,#30628,#30629,#30630,#30631,#30632,#30633,#30634,#30635,#30636,#30637,
#30638,#30639,#30640,#30641,#30642,#30643,#30644,#30645,#30646,#30647,#30648,
#30649,#30650,#30651,#30652,#30653,#30654,#30655,#30656,#30657,#30658,#30659,
#30660,#30661,#30662,#30663,#30664,#30665,#30666,#30667,#30668,#30669,#30670,
#30671,#30672,#30673,#30674,#30675,#30676,#30677,#30678,#30679,#30680,#30681,
#30682,#30683,#30684,#30685,#30686,#30687,#30688,#30689,#30690,#30691,#30692,
#30693,#30694,#30695,#30696,#30697,#30698,#30699,#30700,#30701,#30702,#30703,
#30704,#30705,#30706,#30707,#30708,#30709,#30710,#30711,#30712,#30713,#30714,
#30715,#30716,#30717,#30718,#30719,#30720,#30721,#30722,#30723,#30724,#30725,
#30726,#30727,#30728,#30729,#30730,#30731,#30732,#30733,#30734,#30735,#30736,
#30737,#30738,#30739)),.UNSPECIFIED.,.T.,.F.,.F.)
B_SPLINE_SURFACE_WITH_KNOTS((4,3,4),(4,2,2,2,2,2,2,2,2,2,2,2,2,2,2,2,2,
2,2,2,2,2,2,2,2,2,2,2,2,2,2,2,2,2,2,2,2,2,2,2,2,2,2,2,2,2,2,2,2,2,2,2,2,
2,2,2,2,2,2,2,2,2,2,2,2,2,2,2,2,2,2,2,2,2,2,2,2,2,2,2,2,2,2,2,2,2,2,2,2,
2,2,2,2,2,2,2,2,2,2,2,2,2,2,2,2,2,2,2,2,2,2,2,2,2,2,2,2,2,2,2,2,2,2,2,2,
2,2,2,2,2,2,2,2,2,2,2,2,2,2,2,2,2,2,2,2,2,2,2,2,2,2,2,2,2,4),(0.,0.5,1.),
(0.,0.00568181818181819,0.0184659090909091,0.0248579545454546,0.03125,0.0376420454545455,
0.044034090909091,0.0504261363636365,0.0568181818181819,0.0632102272727274,
0.0696022727272729,0.0759943181818183,0.0823863636363638,0.0887784090909093,
0.0951704545454547,0.1015625,0.107954545454546,0.114346590909092,0.120738636363638,
0.127130681818185,0.133522727272731,0.139914772727278,0.146306818181824,
0.152698863636371,0.159090909090917,0.165482954545461,0.171875000000006,
0.17826704545455,0.184659090909095,0.19105113636364,0.197443181818184,0.203835227272728,
0.210227272727273,0.216619318181819,0.223011363636364,0.22940340909091,
0.235795454545455,0.2421875,0.248579545454546,0.254971590909091,0.261363636363637,
0.267755681818182,0.274147727272728,0.280539772727273,0.286931818181819,
0.293323863636364,0.29971590909091,0.306107954545455,0.3125,0.318892045454546,
0.325284090909092,0.331676136363637,0.338068181818183,0.344460227272728,
0.350852272727274,0.357244318181819,0.363636363636365,0.37002840909091,
0.376420454545456,0.3828125,0.389204545454547,0.395596590909092,0.401988636363638,
0.408380681818183,0.414772727272729,0.421164772727273,0.427556818181818,
0.433948863636362,0.440340909090907,0.446732954545451,0.453125,0.45951704545454,
0.465909090909084,0.472301136363631,0.478693181818177,0.485085227272724,
0.49147727272727,0.497869318181817,0.504261363636363,0.51065340909091,0.517045454545456,
0.5234375,0.529829545454547,0.536221590909093,0.542613636363638,0.549005681818184,
0.555397727272729,0.561789772727275,0.56818181818182,0.574573863636366,
0.580965909090911,0.587357954545456,0.59375,0.600142045454547,0.606534090909093,
0.612926136363638,0.619318181818184,0.625710227272729,0.632102272727275,
0.63849431818182,0.644886363636365,0.651278409090911,0.657670454545456,
0.6640625,0.670454545454547,0.676846590909094,0.68323863636364,0.689630681818186,
0.696022727272733,0.702414772727279,0.708806818181825,0.715198863636372,
0.721590909090918,0.727982954545463,0.734375,0.740767045454552,0.747159090909096,
0.753551136363641,0.759943181818185,0.766335227272729,0.772727272727274,
0.779119318181819,0.785511363636365,0.79190340909091,0.798295454545456,
0.8046875,0.811079545454546,0.817471590909092,0.823863636363637,0.830255681818183,
0.836647727272728,0.843039772727274,0.849431818181819,0.855823863636364,
0.86221590909091,0.868607954545455,0.875,0.881392045454546,0.887784090909092,
0.894176136363637,0.900568181818182,0.906960227272728,0.913352272727273,
0.919744318181819,0.926136363636364,0.932528409090909,0.938920454545455,
0.9453125,0.951704545454546,0.958096590909091,0.964488636363636,0.970880681818182,
0.977272727272727,0.988636363636364,1.),.UNSPECIFIED.)
GEOMETRIC_REPRESENTATION_ITEM()
RATIONAL_B_SPLINE_SURFACE(((1.,1.,1.,1.,1.,1.,1.,1.,1.,1.,1.,1.,1.,1.,1.,
1.,1.,1.,1.,1.,1.,1.,1.,1.,1.,1.,1.,1.,1.,1.,1.,1.,1.,1.,1.,1.,1.,1.,1.,
1.,1.,1.,1.,1.,1.,1.,1.,1.,1.,1.,1.,1.,1.,1.,1.,1.,1.,1.,1.,1.,1.,1.,1.,
1.,1.,1.,1.,1.,1.,1.,1.,1.,1.,1.,1.,1.,1.,1.,1.,1.,1.,1.,1.,1.,1.,1.,1.,
1.,1.,1.,1.,1.,1.,1.,1.,1.,1.,1.,1.,1.,1.,1.,1.,1.,1.,1.,1.,1.,1.,1.,1.,
1.,1.,1.,1.,1.,1.,1.,1.,1.,1.,1.,1.,1.,1.,1.,1.,1.,1.,1.,1.,1.,1.,1.,1.,
1.,1.,1.,1.,1.,1.,1.,1.,1.,1.,1.,1.,1.,1.,1.,1.,1.,1.,1.,1.,1.,1.,1.,1.,
1.,1.,1.,1.,1.,1.,1.,1.,1.,1.,1.,1.,1.,1.,1.,1.,1.,1.,1.,1.,1.,1.,1.,1.,
1.,1.,1.,1.,1.,1.,1.,1.,1.,1.,1.,1.,1.,1.,1.,1.,1.,1.,1.,1.,1.,1.,1.,1.,
1.,1.,1.,1.,1.,1.,1.,1.,1.,1.,1.,1.,1.,1.,1.,1.,1.,1.,1.,1.,1.,1.,1.,1.,
1.,1.,1.,1.,1.,1.,1.,1.,1.,1.,1.,1.,1.,1.,1.,1.,1.,1.,1.,1.,1.,1.,1.,1.,
1.,1.,1.,1.,1.,1.,1.,1.,1.,1.,1.,1.,1.,1.,1.,1.,1.,1.,1.,1.,1.,1.,1.,1.,
1.,1.,1.,1.,1.,1.,1.,1.,1.,1.,1.,1.,1.,1.,1.,1.,1.,1.,1.,1.,1.,1.,1.,1.,
1.,1.,1.,1.,1.,1.,1.),(0.333333333333334,0.333333333333334,0.333333333333334,
0.333333333333334,0.333333333333334,0.333333333333334,0.333333333333334,
0.333333333333334,0.333333333333334,0.333333333333334,0.333333333333334,
0.333333333333334,0.333333333333334,0.333333333333334,0.333333333333334,
0.333333333333334,0.333333333333334,0.333333333333334,0.333333333333334,
0.333333333333334,0.333333333333334,0.333333333333334,0.333333333333334,
0.333333333333334,0.333333333333334,0.333333333333334,0.333333333333334,
0.333333333333334,0.333333333333334,0.333333333333334,0.333333333333334,
0.333333333333334,0.333333333333334,0.333333333333334,0.333333333333334,
0.333333333333334,0.333333333333334,0.333333333333334,0.333333333333334,
0.333333333333334,0.333333333333334,0.333333333333334,0.333333333333334,
0.333333333333334,0.333333333333334,0.333333333333334,0.333333333333334,
0.333333333333334,0.333333333333334,0.333333333333334,0.333333333333334,
0.333333333333334,0.333333333333334,0.333333333333334,0.333333333333334,
0.333333333333334,0.333333333333334,0.333333333333334,0.333333333333334,
0.333333333333334,0.333333333333334,0.333333333333334,0.333333333333334,
0.333333333333334,0.333333333333334,0.333333333333334,0.333333333333334,
0.333333333333334,0.333333333333334,0.333333333333334,0.333333333333334,
0.333333333333334,0.333333333333334,0.333333333333334,0.333333333333334,
0.333333333333334,0.333333333333334,0.333333333333334,0.333333333333334,
0.333333333333334,0.333333333333334,0.333333333333334,0.333333333333334,
0.333333333333334,0.333333333333334,0.333333333333334,0.333333333333334,
0.333333333333334,0.333333333333334,0.333333333333334,0.333333333333334,
0.333333333333334,0.333333333333334,0.333333333333334,0.333333333333334,
0.333333333333334,0.333333333333334,0.333333333333334,0.333333333333334,
0.333333333333334,0.333333333333334,0.333333333333334,0.333333333333334,
0.333333333333334,0.333333333333334,0.333333333333334,0.333333333333334,
0.333333333333334,0.333333333333334,0.333333333333334,0.333333333333334,
0.333333333333334,0.333333333333334,0.333333333333334,0.333333333333334,
0.333333333333334,0.333333333333334,0.333333333333334,0.333333333333334,
0.333333333333334,0.333333333333334,0.333333333333334,0.333333333333334,
0.333333333333334,0.333333333333334,0.333333333333334,0.333333333333334,
0.333333333333334,0.333333333333334,0.333333333333334,0.333333333333334,
0.333333333333334,0.333333333333334,0.333333333333334,0.333333333333334,
0.333333333333334,0.333333333333334,0.333333333333334,0.333333333333334,
0.333333333333334,0.333333333333334,0.333333333333334,0.333333333333334,
0.333333333333334,0.333333333333334,0.333333333333334,0.333333333333334,
0.333333333333334,0.333333333333334,0.333333333333334,0.333333333333334,
0.333333333333334,0.333333333333334,0.333333333333334,0.333333333333334,
0.333333333333334,0.333333333333334,0.333333333333334,0.333333333333334,
0.333333333333334,0.333333333333334,0.333333333333334,0.333333333333334,
0.333333333333334,0.333333333333334,0.333333333333334,0.333333333333334,
0.333333333333334,0.333333333333334,0.333333333333334,0.333333333333334,
0.333333333333334,0.333333333333334,0.333333333333334,0.333333333333334,
0.333333333333334,0.333333333333334,0.333333333333334,0.333333333333334,
0.333333333333334,0.333333333333334,0.333333333333334,0.333333333333334,
0.333333333333334,0.333333333333334,0.333333333333334,0.333333333333334,
0.333333333333334,0.333333333333334,0.333333333333334,0.333333333333334,
0.333333333333334,0.333333333333334,0.333333333333334,0.333333333333334,
0.333333333333334,0.333333333333334,0.333333333333334,0.333333333333334,
0.333333333333334,0.333333333333334,0.333333333333334,0.333333333333334,
0.333333333333334,0.333333333333334,0.333333333333334,0.333333333333334,
0.333333333333334,0.333333333333334,0.333333333333334,0.333333333333334,
0.333333333333334,0.333333333333334,0.333333333333334,0.333333333333334,
0.333333333333334,0.333333333333334,0.333333333333334,0.333333333333334,
0.333333333333334,0.333333333333334,0.333333333333334,0.333333333333334,
0.333333333333334,0.333333333333334,0.333333333333334,0.333333333333334,
0.333333333333334,0.333333333333334,0.333333333333334,0.333333333333334,
0.333333333333334,0.333333333333334,0.333333333333334,0.333333333333334,
0.333333333333334,0.333333333333334,0.333333333333334,0.333333333333334,
0.333333333333334,0.333333333333334,0.333333333333334,0.333333333333334,
0.333333333333334,0.333333333333334,0.333333333333334,0.333333333333334,
0.333333333333334,0.333333333333334,0.333333333333334,0.333333333333334,
0.333333333333334,0.333333333333334,0.333333333333334,0.333333333333334,
0.333333333333334,0.333333333333334,0.333333333333334,0.333333333333334,
0.333333333333334,0.333333333333334,0.333333333333334,0.333333333333334,
0.333333333333334,0.333333333333334,0.333333333333334,0.333333333333334,
0.333333333333334,0.333333333333334,0.333333333333334,0.333333333333334,
0.333333333333334,0.333333333333334,0.333333333333334,0.333333333333334,
0.333333333333334,0.333333333333334,0.333333333333334,0.333333333333334,
0.333333333333334,0.333333333333334,0.333333333333334,0.333333333333334,
0.333333333333334,0.333333333333334,0.333333333333334,0.333333333333334,
0.333333333333334,0.333333333333334,0.333333333333334,0.333333333333334,
0.333333333333334,0.333333333333334,0.333333333333334,0.333333333333334,
0.333333333333334,0.333333333333334,0.333333333333334,0.333333333333334,
0.333333333333334,0.333333333333334,0.333333333333334,0.333333333333334,
0.333333333333334,0.333333333333334,0.333333333333334,0.333333333333334,
0.333333333333334,0.333333333333334,0.333333333333334),(0.333333333333334,
0.333333333333334,0.333333333333334,0.333333333333334,0.333333333333334,
0.333333333333334,0.333333333333334,0.333333333333334,0.333333333333334,
0.333333333333334,0.333333333333334,0.333333333333334,0.333333333333334,
0.333333333333334,0.333333333333334,0.333333333333334,0.333333333333334,
0.333333333333334,0.333333333333334,0.333333333333334,0.333333333333334,
0.333333333333334,0.333333333333334,0.333333333333334,0.333333333333334,
0.333333333333334,0.333333333333334,0.333333333333334,0.333333333333334,
0.333333333333334,0.333333333333334,0.333333333333334,0.333333333333334,
0.333333333333334,0.333333333333334,0.333333333333334,0.333333333333334,
0.333333333333334,0.333333333333334,0.333333333333334,0.333333333333334,
0.333333333333334,0.333333333333334,0.333333333333334,0.333333333333334,
0.333333333333334,0.333333333333334,0.333333333333334,0.333333333333334,
0.333333333333334,0.333333333333334,0.333333333333334,0.333333333333334,
0.333333333333334,0.333333333333334,0.333333333333334,0.333333333333334,
0.333333333333334,0.333333333333334,0.333333333333334,0.333333333333334,
0.333333333333334,0.333333333333334,0.333333333333334,0.333333333333334,
0.333333333333334,0.333333333333334,0.333333333333334,0.333333333333334,
0.333333333333334,0.333333333333334,0.333333333333334,0.333333333333334,
0.333333333333334,0.333333333333334,0.333333333333334,0.333333333333334,
0.333333333333334,0.333333333333334,0.333333333333334,0.333333333333334,
0.333333333333334,0.333333333333334,0.333333333333334,0.333333333333334,
0.333333333333334,0.333333333333334,0.333333333333334,0.333333333333334,
0.333333333333334,0.333333333333334,0.333333333333334,0.333333333333334,
0.333333333333334,0.333333333333334,0.333333333333334,0.333333333333334,
0.333333333333334,0.333333333333334,0.333333333333334,0.333333333333334,
0.333333333333334,0.333333333333334,0.333333333333334,0.333333333333334,
0.333333333333334,0.333333333333334,0.333333333333334,0.333333333333334,
0.333333333333334,0.333333333333334,0.333333333333334,0.333333333333334,
0.333333333333334,0.333333333333334,0.333333333333334,0.333333333333334,
0.333333333333334,0.333333333333334,0.333333333333334,0.333333333333334,
0.333333333333334,0.333333333333334,0.333333333333334,0.333333333333334,
0.333333333333334,0.333333333333334,0.333333333333334,0.333333333333334,
0.333333333333334,0.333333333333334,0.333333333333334,0.333333333333334,
0.333333333333334,0.333333333333334,0.333333333333334,0.333333333333334,
0.333333333333334,0.333333333333334,0.333333333333334,0.333333333333334,
0.333333333333334,0.333333333333334,0.333333333333334,0.333333333333334,
0.333333333333334,0.333333333333334,0.333333333333334,0.333333333333334,
0.333333333333334,0.333333333333334,0.333333333333334,0.333333333333334,
0.333333333333334,0.333333333333334,0.333333333333334,0.333333333333334,
0.333333333333334,0.333333333333334,0.333333333333334,0.333333333333334,
0.333333333333334,0.333333333333334,0.333333333333334,0.333333333333334,
0.333333333333334,0.333333333333334,0.333333333333334,0.333333333333334,
0.333333333333334,0.333333333333334,0.333333333333334,0.333333333333334,
0.333333333333334,0.333333333333334,0.333333333333334,0.333333333333334,
0.333333333333334,0.333333333333334,0.333333333333334,0.333333333333334,
0.333333333333334,0.333333333333334,0.333333333333334,0.333333333333334,
0.333333333333334,0.333333333333334,0.333333333333334,0.333333333333334,
0.333333333333334,0.333333333333334,0.333333333333334,0.333333333333334,
0.333333333333334,0.333333333333334,0.333333333333334,0.333333333333334,
0.333333333333334,0.333333333333334,0.333333333333334,0.333333333333334,
0.333333333333334,0.333333333333334,0.333333333333334,0.333333333333334,
0.333333333333334,0.333333333333334,0.333333333333334,0.333333333333334,
0.333333333333334,0.333333333333334,0.333333333333334,0.333333333333334,
0.333333333333334,0.333333333333334,0.333333333333334,0.333333333333334,
0.333333333333334,0.333333333333334,0.333333333333334,0.333333333333334,
0.333333333333334,0.333333333333334,0.333333333333334,0.333333333333334,
0.333333333333334,0.333333333333334,0.333333333333334,0.333333333333334,
0.333333333333334,0.333333333333334,0.333333333333334,0.333333333333334,
0.333333333333334,0.333333333333334,0.333333333333334,0.333333333333334,
0.333333333333334,0.333333333333334,0.333333333333334,0.333333333333334,
0.333333333333334,0.333333333333334,0.333333333333334,0.333333333333334,
0.333333333333334,0.333333333333334,0.333333333333334,0.333333333333334,
0.333333333333334,0.333333333333334,0.333333333333334,0.333333333333334,
0.333333333333334,0.333333333333334,0.333333333333334,0.333333333333334,
0.333333333333334,0.333333333333334,0.333333333333334,0.333333333333334,
0.333333333333334,0.333333333333334,0.333333333333334,0.333333333333334,
0.333333333333334,0.333333333333334,0.333333333333334,0.333333333333334,
0.333333333333334,0.333333333333334,0.333333333333334,0.333333333333334,
0.333333333333334,0.333333333333334,0.333333333333334,0.333333333333334,
0.333333333333334,0.333333333333334,0.333333333333334,0.333333333333334,
0.333333333333334,0.333333333333334,0.333333333333334,0.333333333333334,
0.333333333333334,0.333333333333334,0.333333333333334,0.333333333333334,
0.333333333333334,0.333333333333334,0.333333333333334,0.333333333333334,
0.333333333333334,0.333333333333334,0.333333333333334,0.333333333333334,
0.333333333333334,0.333333333333334,0.333333333333334,0.333333333333334,
0.333333333333334,0.333333333333334,0.333333333333334,0.333333333333334,
0.333333333333334,0.333333333333334,0.333333333333334,0.333333333333334,
0.333333333333334),(1.,1.,1.,1.,1.,1.,1.,1.,1.,1.,1.,1.,1.,1.,1.,1.,1.,
1.,1.,1.,1.,1.,1.,1.,1.,1.,1.,1.,1.,1.,1.,1.,1.,1.,1.,1.,1.,1.,1.,1.,1.,
1.,1.,1.,1.,1.,1.,1.,1.,1.,1.,1.,1.,1.,1.,1.,1.,1.,1.,1.,1.,1.,1.,1.,1.,
1.,1.,1.,1.,1.,1.,1.,1.,1.,1.,1.,1.,1.,1.,1.,1.,1.,1.,1.,1.,1.,1.,1.,1.,
1.,1.,1.,1.,1.,1.,1.,1.,1.,1.,1.,1.,1.,1.,1.,1.,1.,1.,1.,1.,1.,1.,1.,1.,
1.,1.,1.,1.,1.,1.,1.,1.,1.,1.,1.,1.,1.,1.,1.,1.,1.,1.,1.,1.,1.,1.,1.,1.,
1.,1.,1.,1.,1.,1.,1.,1.,1.,1.,1.,1.,1.,1.,1.,1.,1.,1.,1.,1.,1.,1.,1.,1.,
1.,1.,1.,1.,1.,1.,1.,1.,1.,1.,1.,1.,1.,1.,1.,1.,1.,1.,1.,1.,1.,1.,1.,1.,
1.,1.,1.,1.,1.,1.,1.,1.,1.,1.,1.,1.,1.,1.,1.,1.,1.,1.,1.,1.,1.,1.,1.,1.,
1.,1.,1.,1.,1.,1.,1.,1.,1.,1.,1.,1.,1.,1.,1.,1.,1.,1.,1.,1.,1.,1.,1.,1.,
1.,1.,1.,1.,1.,1.,1.,1.,1.,1.,1.,1.,1.,1.,1.,1.,1.,1.,1.,1.,1.,1.,1.,1.,
1.,1.,1.,1.,1.,1.,1.,1.,1.,1.,1.,1.,1.,1.,1.,1.,1.,1.,1.,1.,1.,1.,1.,1.,
1.,1.,1.,1.,1.,1.,1.,1.,1.,1.,1.,1.,1.,1.,1.,1.,1.,1.,1.,1.,1.,1.,1.,1.,
1.,1.,1.,1.,1.),(0.333333333333334,0.333333333333334,0.333333333333334,
0.333333333333334,0.333333333333334,0.333333333333334,0.333333333333334,
0.333333333333334,0.333333333333334,0.333333333333334,0.333333333333334,
0.333333333333334,0.333333333333334,0.333333333333334,0.333333333333334,
0.333333333333334,0.333333333333334,0.333333333333334,0.333333333333334,
0.333333333333334,0.333333333333334,0.333333333333334,0.333333333333334,
0.333333333333334,0.333333333333334,0.333333333333334,0.333333333333334,
0.333333333333334,0.333333333333334,0.333333333333334,0.333333333333334,
0.333333333333334,0.333333333333334,0.333333333333334,0.333333333333334,
0.333333333333334,0.333333333333334,0.333333333333334,0.333333333333334,
0.333333333333334,0.333333333333334,0.333333333333334,0.333333333333334,
0.333333333333334,0.333333333333334,0.333333333333334,0.333333333333334,
0.333333333333334,0.333333333333334,0.333333333333334,0.333333333333334,
0.333333333333334,0.333333333333334,0.333333333333334,0.333333333333334,
0.333333333333334,0.333333333333334,0.333333333333334,0.333333333333334,
0.333333333333334,0.333333333333334,0.333333333333334,0.333333333333334,
0.333333333333334,0.333333333333334,0.333333333333334,0.333333333333334,
0.333333333333334,0.333333333333334,0.333333333333334,0.333333333333334,
0.333333333333334,0.333333333333334,0.333333333333334,0.333333333333334,
0.333333333333334,0.333333333333334,0.333333333333334,0.333333333333334,
0.333333333333334,0.333333333333334,0.333333333333334,0.333333333333334,
0.333333333333334,0.333333333333334,0.333333333333334,0.333333333333334,
0.333333333333334,0.333333333333334,0.333333333333334,0.333333333333334,
0.333333333333334,0.333333333333334,0.333333333333334,0.333333333333334,
0.333333333333334,0.333333333333334,0.333333333333334,0.333333333333334,
0.333333333333334,0.333333333333334,0.333333333333334,0.333333333333334,
0.333333333333334,0.333333333333334,0.333333333333334,0.333333333333334,
0.333333333333334,0.333333333333334,0.333333333333334,0.333333333333334,
0.333333333333334,0.333333333333334,0.333333333333334,0.333333333333334,
0.333333333333334,0.333333333333334,0.333333333333334,0.333333333333334,
0.333333333333334,0.333333333333334,0.333333333333334,0.333333333333334,
0.333333333333334,0.333333333333334,0.333333333333334,0.333333333333334,
0.333333333333334,0.333333333333334,0.333333333333334,0.333333333333334,
0.333333333333334,0.333333333333334,0.333333333333334,0.333333333333334,
0.333333333333334,0.333333333333334,0.333333333333334,0.333333333333334,
0.333333333333334,0.333333333333334,0.333333333333334,0.333333333333334,
0.333333333333334,0.333333333333334,0.333333333333334,0.333333333333334,
0.333333333333334,0.333333333333334,0.333333333333334,0.333333333333334,
0.333333333333334,0.333333333333334,0.333333333333334,0.333333333333334,
0.333333333333334,0.333333333333334,0.333333333333334,0.333333333333334,
0.333333333333334,0.333333333333334,0.333333333333334,0.333333333333334,
0.333333333333334,0.333333333333334,0.333333333333334,0.333333333333334,
0.333333333333334,0.333333333333334,0.333333333333334,0.333333333333334,
0.333333333333334,0.333333333333334,0.333333333333334,0.333333333333334,
0.333333333333334,0.333333333333334,0.333333333333334,0.333333333333334,
0.333333333333334,0.333333333333334,0.333333333333334,0.333333333333334,
0.333333333333334,0.333333333333334,0.333333333333334,0.333333333333334,
0.333333333333334,0.333333333333334,0.333333333333334,0.333333333333334,
0.333333333333334,0.333333333333334,0.333333333333334,0.333333333333334,
0.333333333333334,0.333333333333334,0.333333333333334,0.333333333333334,
0.333333333333334,0.333333333333334,0.333333333333334,0.333333333333334,
0.333333333333334,0.333333333333334,0.333333333333334,0.333333333333334,
0.333333333333334,0.333333333333334,0.333333333333334,0.333333333333334,
0.333333333333334,0.333333333333334,0.333333333333334,0.333333333333334,
0.333333333333334,0.333333333333334,0.333333333333334,0.333333333333334,
0.333333333333334,0.333333333333334,0.333333333333334,0.333333333333334,
0.333333333333334,0.333333333333334,0.333333333333334,0.333333333333334,
0.333333333333334,0.333333333333334,0.333333333333334,0.333333333333334,
0.333333333333334,0.333333333333334,0.333333333333334,0.333333333333334,
0.333333333333334,0.333333333333334,0.333333333333334,0.333333333333334,
0.333333333333334,0.333333333333334,0.333333333333334,0.333333333333334,
0.333333333333334,0.333333333333334,0.333333333333334,0.333333333333334,
0.333333333333334,0.333333333333334,0.333333333333334,0.333333333333334,
0.333333333333334,0.333333333333334,0.333333333333334,0.333333333333334,
0.333333333333334,0.333333333333334,0.333333333333334,0.333333333333334,
0.333333333333334,0.333333333333334,0.333333333333334,0.333333333333334,
0.333333333333334,0.333333333333334,0.333333333333334,0.333333333333334,
0.333333333333334,0.333333333333334,0.333333333333334,0.333333333333334,
0.333333333333334,0.333333333333334,0.333333333333334,0.333333333333334,
0.333333333333334,0.333333333333334,0.333333333333334,0.333333333333334,
0.333333333333334,0.333333333333334,0.333333333333334,0.333333333333334,
0.333333333333334,0.333333333333334,0.333333333333334,0.333333333333334,
0.333333333333334,0.333333333333334,0.333333333333334,0.333333333333334,
0.333333333333334,0.333333333333334,0.333333333333334,0.333333333333334,
0.333333333333334,0.333333333333334,0.333333333333334,0.333333333333334,
0.333333333333334,0.333333333333334,0.333333333333334,0.333333333333334,
0.333333333333334,0.333333333333334,0.333333333333334,0.333333333333334,
0.333333333333334,0.333333333333334,0.333333333333334),(0.333333333333334,
0.333333333333334,0.333333333333334,0.333333333333334,0.333333333333334,
0.333333333333334,0.333333333333334,0.333333333333334,0.333333333333334,
0.333333333333334,0.333333333333334,0.333333333333334,0.333333333333334,
0.333333333333334,0.333333333333334,0.333333333333334,0.333333333333334,
0.333333333333334,0.333333333333334,0.333333333333334,0.333333333333334,
0.333333333333334,0.333333333333334,0.333333333333334,0.333333333333334,
0.333333333333334,0.333333333333334,0.333333333333334,0.333333333333334,
0.333333333333334,0.333333333333334,0.333333333333334,0.333333333333334,
0.333333333333334,0.333333333333334,0.333333333333334,0.333333333333334,
0.333333333333334,0.333333333333334,0.333333333333334,0.333333333333334,
0.333333333333334,0.333333333333334,0.333333333333334,0.333333333333334,
0.333333333333334,0.333333333333334,0.333333333333334,0.333333333333334,
0.333333333333334,0.333333333333334,0.333333333333334,0.333333333333334,
0.333333333333334,0.333333333333334,0.333333333333334,0.333333333333334,
0.333333333333334,0.333333333333334,0.333333333333334,0.333333333333334,
0.333333333333334,0.333333333333334,0.333333333333334,0.333333333333334,
0.333333333333334,0.333333333333334,0.333333333333334,0.333333333333334,
0.333333333333334,0.333333333333334,0.333333333333334,0.333333333333334,
0.333333333333334,0.333333333333334,0.333333333333334,0.333333333333334,
0.333333333333334,0.333333333333334,0.333333333333334,0.333333333333334,
0.333333333333334,0.333333333333334,0.333333333333334,0.333333333333334,
0.333333333333334,0.333333333333334,0.333333333333334,0.333333333333334,
0.333333333333334,0.333333333333334,0.333333333333334,0.333333333333334,
0.333333333333334,0.333333333333334,0.333333333333334,0.333333333333334,
0.333333333333334,0.333333333333334,0.333333333333334,0.333333333333334,
0.333333333333334,0.333333333333334,0.333333333333334,0.333333333333334,
0.333333333333334,0.333333333333334,0.333333333333334,0.333333333333334,
0.333333333333334,0.333333333333334,0.333333333333334,0.333333333333334,
0.333333333333334,0.333333333333334,0.333333333333334,0.333333333333334,
0.333333333333334,0.333333333333334,0.333333333333334,0.333333333333334,
0.333333333333334,0.333333333333334,0.333333333333334,0.333333333333334,
0.333333333333334,0.333333333333334,0.333333333333334,0.333333333333334,
0.333333333333334,0.333333333333334,0.333333333333334,0.333333333333334,
0.333333333333334,0.333333333333334,0.333333333333334,0.333333333333334,
0.333333333333334,0.333333333333334,0.333333333333334,0.333333333333334,
0.333333333333334,0.333333333333334,0.333333333333334,0.333333333333334,
0.333333333333334,0.333333333333334,0.333333333333334,0.333333333333334,
0.333333333333334,0.333333333333334,0.333333333333334,0.333333333333334,
0.333333333333334,0.333333333333334,0.333333333333334,0.333333333333334,
0.333333333333334,0.333333333333334,0.333333333333334,0.333333333333334,
0.333333333333334,0.333333333333334,0.333333333333334,0.333333333333334,
0.333333333333334,0.333333333333334,0.333333333333334,0.333333333333334,
0.333333333333334,0.333333333333334,0.333333333333334,0.333333333333334,
0.333333333333334,0.333333333333334,0.333333333333334,0.333333333333334,
0.333333333333334,0.333333333333334,0.333333333333334,0.333333333333334,
0.333333333333334,0.333333333333334,0.333333333333334,0.333333333333334,
0.333333333333334,0.333333333333334,0.333333333333334,0.333333333333334,
0.333333333333334,0.333333333333334,0.333333333333334,0.333333333333334,
0.333333333333334,0.333333333333334,0.333333333333334,0.333333333333334,
0.333333333333334,0.333333333333334,0.333333333333334,0.333333333333334,
0.333333333333334,0.333333333333334,0.333333333333334,0.333333333333334,
0.333333333333334,0.333333333333334,0.333333333333334,0.333333333333334,
0.333333333333334,0.333333333333334,0.333333333333334,0.333333333333334,
0.333333333333334,0.333333333333334,0.333333333333334,0.333333333333334,
0.333333333333334,0.333333333333334,0.333333333333334,0.333333333333334,
0.333333333333334,0.333333333333334,0.333333333333334,0.333333333333334,
0.333333333333334,0.333333333333334,0.333333333333334,0.333333333333334,
0.333333333333334,0.333333333333334,0.333333333333334,0.333333333333334,
0.333333333333334,0.333333333333334,0.333333333333334,0.333333333333334,
0.333333333333334,0.333333333333334,0.333333333333334,0.333333333333334,
0.333333333333334,0.333333333333334,0.333333333333334,0.333333333333334,
0.333333333333334,0.333333333333334,0.333333333333334,0.333333333333334,
0.333333333333334,0.333333333333334,0.333333333333334,0.333333333333334,
0.333333333333334,0.333333333333334,0.333333333333334,0.333333333333334,
0.333333333333334,0.333333333333334,0.333333333333334,0.333333333333334,
0.333333333333334,0.333333333333334,0.333333333333334,0.333333333333334,
0.333333333333334,0.333333333333334,0.333333333333334,0.333333333333334,
0.333333333333334,0.333333333333334,0.333333333333334,0.333333333333334,
0.333333333333334,0.333333333333334,0.333333333333334,0.333333333333334,
0.333333333333334,0.333333333333334,0.333333333333334,0.333333333333334,
0.333333333333334,0.333333333333334,0.333333333333334,0.333333333333334,
0.333333333333334,0.333333333333334,0.333333333333334,0.333333333333334,
0.333333333333334,0.333333333333334,0.333333333333334,0.333333333333334,
0.333333333333334,0.333333333333334,0.333333333333334,0.333333333333334,
0.333333333333334,0.333333333333334,0.333333333333334,0.333333333333334,
0.333333333333334,0.333333333333334,0.333333333333334,0.333333333333334,
0.333333333333334,0.333333333333334,0.333333333333334,0.333333333333334,
0.333333333333334),(1.,1.,1.,1.,1.,1.,1.,1.,1.,1.,1.,1.,1.,1.,1.,1.,1.,
1.,1.,1.,1.,1.,1.,1.,1.,1.,1.,1.,1.,1.,1.,1.,1.,1.,1.,1.,1.,1.,1.,1.,1.,
1.,1.,1.,1.,1.,1.,1.,1.,1.,1.,1.,1.,1.,1.,1.,1.,1.,1.,1.,1.,1.,1.,1.,1.,
1.,1.,1.,1.,1.,1.,1.,1.,1.,1.,1.,1.,1.,1.,1.,1.,1.,1.,1.,1.,1.,1.,1.,1.,
1.,1.,1.,1.,1.,1.,1.,1.,1.,1.,1.,1.,1.,1.,1.,1.,1.,1.,1.,1.,1.,1.,1.,1.,
1.,1.,1.,1.,1.,1.,1.,1.,1.,1.,1.,1.,1.,1.,1.,1.,1.,1.,1.,1.,1.,1.,1.,1.,
1.,1.,1.,1.,1.,1.,1.,1.,1.,1.,1.,1.,1.,1.,1.,1.,1.,1.,1.,1.,1.,1.,1.,1.,
1.,1.,1.,1.,1.,1.,1.,1.,1.,1.,1.,1.,1.,1.,1.,1.,1.,1.,1.,1.,1.,1.,1.,1.,
1.,1.,1.,1.,1.,1.,1.,1.,1.,1.,1.,1.,1.,1.,1.,1.,1.,1.,1.,1.,1.,1.,1.,1.,
1.,1.,1.,1.,1.,1.,1.,1.,1.,1.,1.,1.,1.,1.,1.,1.,1.,1.,1.,1.,1.,1.,1.,1.,
1.,1.,1.,1.,1.,1.,1.,1.,1.,1.,1.,1.,1.,1.,1.,1.,1.,1.,1.,1.,1.,1.,1.,1.,
1.,1.,1.,1.,1.,1.,1.,1.,1.,1.,1.,1.,1.,1.,1.,1.,1.,1.,1.,1.,1.,1.,1.,1.,
1.,1.,1.,1.,1.,1.,1.,1.,1.,1.,1.,1.,1.,1.,1.,1.,1.,1.,1.,1.,1.,1.,1.,1.,
1.,1.,1.,1.,1.)))
REPRESENTATION_ITEM('')
SURFACE()
);
#12826=ADVANCED_FACE('',(#11756),#1240,.F.);
#12827=ADVANCED_FACE('',(#11757),#1241,.T.);
#12828=ADVANCED_FACE('',(#11758,#11759),#12674,.T.);
#13506=CLOSED_SHELL('',(#12826,#12827,#12828));
#13533=STYLED_ITEM('',(#13560),#13723);
#13560=PRESENTATION_STYLE_ASSIGNMENT((#13587));
#13587=SURFACE_STYLE_USAGE(.BOTH.,#13614);
#13614=SURFACE_SIDE_STYLE('',(#13641));
#13641=SURFACE_STYLE_FILL_AREA(#13668);
#13668=FILL_AREA_STYLE('',(#13695));
#13695=FILL_AREA_STYLE_COLOUR('',#60);
#13723=MANIFOLD_SOLID_BREP('spring',#13506);
#13751=SHAPE_DEFINITION_REPRESENTATION(#45532,#13779);
#13779=SHAPE_REPRESENTATION('spring',(#13802),#45469);
#13802=AXIS2_PLACEMENT_3D('',#19109,#15295,#15296);
#14004=AXIS2_PLACEMENT_3D('',#28564,#15747,#15748);
#14005=AXIS2_PLACEMENT_3D('',#28565,#15749,#15750);
#14006=AXIS2_PLACEMENT_3D('',#28567,#15751,#15752);
#14007=AXIS2_PLACEMENT_3D('',#28568,#15753,#15754);
#15295=DIRECTION('',(0.,0.,1.));
#15296=DIRECTION('',(1.,0.,0.));
#15747=DIRECTION('',(-7.77379789764059E-15,0.999160784934254,0.0409600518745398));
#15748=DIRECTION('',(0.,-0.0409600518745398,0.999160784934254));
#15749=DIRECTION('',(-7.77379789764059E-15,0.999160784934254,0.0409600518745398));
#15750=DIRECTION('',(0.,-0.0409600518745399,0.999160784934254));
#15751=DIRECTION('',(1.54365415442519E-13,0.999160784934254,0.040960051874541));
#15752=DIRECTION('',(9.60032442200731E-5,-0.0409600516857843,0.99916078032981));
#15753=DIRECTION('',(1.54365416289552E-13,0.999160784934254,0.040960051874541));
#15754=DIRECTION('',(9.60032442198703E-5,-0.0409600516857843,0.99916078032981));
#19109=CARTESIAN_POINT('',(0.,0.,0.));
#28564=CARTESIAN_POINT('',(-0.006,-4.18502038579405E-17,-0.0146355706936178));
#28565=CARTESIAN_POINT('',(-0.006,-4.18502038579405E-17,-0.0146355706936178));
#28566=CARTESIAN_POINT('',(-0.006,-2.43712308653931E-5,-0.0140410700265819));
#28567=CARTESIAN_POINT('',(-0.006,9.23323236123637E-16,0.00236442930638223));
#28568=CARTESIAN_POINT('',(-0.006,9.23323236123637E-16,0.00236442930638223));
#28569=CARTESIAN_POINT('',(-0.00599994287806969,-2.43712307521178E-5,0.00295892997067845));
#28570=CARTESIAN_POINT('',(-0.006,-2.43712308653931E-5,-0.0140410700265819));
#28571=CARTESIAN_POINT('',(-0.00600309747414711,0.000755994738560391,-0.0140090793492257));
#28572=CARTESIAN_POINT('',(-0.00585022549906422,0.00154554847924553,-0.0139767317091225));
#28573=CARTESIAN_POINT('',(-0.00488277416170381,0.00391156551240249,-0.0138719117580559));
#28574=CARTESIAN_POINT('',(-0.00345414811439852,0.00521522772168569,-0.0137995939835592));
#28575=CARTESIAN_POINT('',(-0.000920416913494161,0.00599387797088215,-0.0136909247186258));
#28576=CARTESIAN_POINT('',(-1.83364399790589E-5,0.00606458475875607,-0.0136547070017816));
#28577=CARTESIAN_POINT('',(0.00173071508355203,0.00581192078991974,-0.013582263622242));
#28578=CARTESIAN_POINT('',(0.00257620709021928,0.0054899026401681,-0.013546041378497));
#28579=CARTESIAN_POINT('',(0.0040496481570146,0.00451412616898593,-0.0134735982934369));
#28580=CARTESIAN_POINT('',(0.00467595743139725,0.00386119227478036,-0.0134373767382566));
#28581=CARTESIAN_POINT('',(0.00559115533267521,0.00234942868328478,-0.0133649337688717));
#28582=CARTESIAN_POINT('',(0.00587789190074464,0.00149118187026969,-0.013328711875432));
#28583=CARTESIAN_POINT('',(0.00605911477020831,-0.000266602851011457,-0.0132562691328768));
#28584=CARTESIAN_POINT('',(0.00595132195371268,-0.00116523586494131,-0.0132200472158988));
#28585=CARTESIAN_POINT('',(0.00536345211542811,-0.00283155473315956,-0.0131476043990316));
#28586=CARTESIAN_POINT('',(0.00488207572844726,-0.00359821831670739,-0.013111382654392));
#28587=CARTESIAN_POINT('',(0.00363763601600018,-0.00485255191712249,-0.0130389394867723));
#28588=CARTESIAN_POINT('',(0.00287504504636738,-0.00534029243914702,-0.0130027180351518));
#28589=CARTESIAN_POINT('',(0.00121351369399411,-0.00594156052931282,-0.0129302744931486));
#28590=CARTESIAN_POINT('',(0.000315825750312525,-0.00605668045304735,-0.0128940532261725));
#28591=CARTESIAN_POINT('',(-0.00144337707403964,-0.00588978902230696,-0.0128216096183549));
#28592=CARTESIAN_POINT('',(-0.00230387638883705,-0.00560996798125232,-0.012785388316591));
#28593=CARTESIAN_POINT('',(-0.00382310259116674,-0.00470721006652816,-0.0127129448611614));
#28594=CARTESIAN_POINT('',(-0.00448099997246373,-0.00408613400852397,-0.0126767233862572));
#28595=CARTESIAN_POINT('',(-0.0054688674143523,-0.00262077375144199,-0.0126042801976742));
#28596=CARTESIAN_POINT('',(-0.00579763556460296,-0.0017778661740937,-0.0125680585008892));
#28597=CARTESIAN_POINT('',(-0.00606464167597128,-3.0946622266283E-5,-0.0124956155817382));
#28598=CARTESIAN_POINT('',(-0.00600111463142179,0.00087169976698755,-0.012459393707512));
#28599=CARTESIAN_POINT('',(-0.00549586755061847,0.00256503164149849,-0.0123869509484387));
#28600=CARTESIAN_POINT('',(-0.0050523880893689,0.00335400980216192,-0.0123507290311181));
#28601=CARTESIAN_POINT('',(-0.00387159456299549,0.00466851979026504,-0.0122782862186558));
#28602=CARTESIAN_POINT('',(-0.00313347130157478,0.00519260976096335,-0.0122420644730658));
#28603=CARTESIAN_POINT('',(-0.00150374624037729,0.00587523641666246,-0.0121696213045038));
#28604=CARTESIAN_POINT('',(-0.000612553833171288,0.00603401898911306,-0.0121333998532844));
#28605=CARTESIAN_POINT('',(0.00115259631366971,0.00595367775238322,-0.012060956311437));
#28606=CARTESIAN_POINT('',(0.00202600631780663,0.00571650438740237,-0.0120247350443508));
#28607=CARTESIAN_POINT('',(0.00358743121515774,0.00488909903514313,-0.0119522914365147));
#28608=CARTESIAN_POINT('',(0.00427534604366821,0.00430127927179916,-0.0119160701347756));
#28609=CARTESIAN_POINT('',(0.00533345753982393,0.00288585701390729,-0.011843626679348));
#28610=CARTESIAN_POINT('',(0.00570359994722143,0.00206029112764935,-0.0118074052044376));
#28611=CARTESIAN_POINT('',(0.00605550136478055,0.000328434275013915,-0.0117349620158554));
#28612=CARTESIAN_POINT('',(0.00603667676489193,-0.000576124907669123,-0.0116987403190736));
#28613=CARTESIAN_POINT('',(0.00561484107606885,-0.00229224694171357,-0.0116262973999176));
#28614=CARTESIAN_POINT('',(0.00521072192138963,-0.00310187271837801,-0.0115900755256951));
#28615=CARTESIAN_POINT('',(0.0040959244307272,-0.0044729576919261,-0.0115176327666191));
#28616=CARTESIAN_POINT('',(0.0033842739627938,-0.00503216622374487,-0.0114814108492998));
#28617=CARTESIAN_POINT('',(0.00179032179752591,-0.00579474497744012,-0.0114089680368375));
#28618=CARTESIAN_POINT('',(0.000907824274980536,-0.0059964734313809,-0.0113727462912467));
#28619=CARTESIAN_POINT('',(-0.000859075264311106,-0.00600346944668868,-0.0113003031226866));
#28620=CARTESIAN_POINT('',(-0.00174319314868272,-0.00580912084620773,-0.0112640816714646));
#28621=CARTESIAN_POINT('',(-0.00334323398092842,-0.00505940150515071,-0.0111916381296202));
#28622=CARTESIAN_POINT('',(-0.0040593972898715,-0.00450604234934652,-0.0111554168625309));
#28623=CARTESIAN_POINT('',(-0.00518533147390755,-0.00314408804019317,-0.0110829732546983));
#28624=CARTESIAN_POINT('',(-0.00559593301943456,-0.00233775978428837,-0.0110467519529574));
#28625=CARTESIAN_POINT('',(-0.00603184192596513,-0.000625158391190649,-0.0109743084975298));
#28626=CARTESIAN_POINT('',(-0.00605787853325042,0.000279212400784205,-0.010938087022621));
#28627=CARTESIAN_POINT('',(-0.00572024012570424,0.00201390634250815,-0.0108656438340358));
#28628=CARTESIAN_POINT('',(-0.00535668865032753,0.00284240619482864,-0.0108294221372547));
#28629=CARTESIAN_POINT('',(-0.00431023182100595,0.00426646668808826,-0.0107569792181002));
#28630=CARTESIAN_POINT('',(-0.00362704403416047,0.0048598136669573,-0.0107207573438761));
#28631=CARTESIAN_POINT('',(-0.00207241394588092,0.00569991648120368,-0.0106483145848017));
#28632=CARTESIAN_POINT('',(-0.00120093480390402,0.00594422095445996,-0.0106120926674817));
#28633=CARTESIAN_POINT('',(0.000563511232301897,0.00603877277129276,-0.0105396498550195));
#28634=CARTESIAN_POINT('',(0.00145603076803849,0.00588742838004165,-0.01050342810943));
#28635=CARTESIAN_POINT('',(0.003091110347539,0.0052177286750386,-0.0104309849408669));
#28636=CARTESIAN_POINT('',(0.00383355477573361,0.00469983671428884,-0.0103947634896458));
#28637=CARTESIAN_POINT('',(0.00502489458107504,0.00339487724234225,-0.0103223199478029));
#28638=CARTESIAN_POINT('',(0.00547478182306626,0.00260957621096752,-0.0102860986807135));
#28639=CARTESIAN_POINT('',(0.00599381202091714,0.000920418142363337,-0.0102136550728794));
#28640=CARTESIAN_POINT('',(0.00606458992024415,1.83375614756708E-5,-0.0101774337711432));
#28641=CARTESIAN_POINT('',(0.00581193305766793,-0.00173071492951537,-0.0101049903157079));
#28642=CARTESIAN_POINT('',(0.00548990002742215,-0.00257620837226416,-0.0100687688408028));
#28643=CARTESIAN_POINT('',(0.00451412418157153,-0.00404964797549366,-0.00999632565221761));
#28644=CARTESIAN_POINT('',(0.00386119324725615,-0.00467595690529434,-0.00996010395543582));
#28645=CARTESIAN_POINT('',(0.00234942884354364,-0.00559115555682603,-0.00988766103628286));
#28646=CARTESIAN_POINT('',(0.00149118157195093,-0.00587789203903946,-0.00985143916205724));
#28647=CARTESIAN_POINT('',(-0.000266602775728381,-0.00605911465611149,-0.00977899640298428));
#28648=CARTESIAN_POINT('',(-0.00116523579238055,-0.00595132192935385,-0.00974277448566356));
#28649=CARTESIAN_POINT('',(-0.0028315547852557,-0.00536345215233157,-0.00967033167320129));
#28650=CARTESIAN_POINT('',(-0.00359821832558892,-0.00488207572751732,-0.00963410992760799));
#28651=CARTESIAN_POINT('',(-0.00485255190132513,-0.00363763601143704,-0.00956166675905256));
#28652=CARTESIAN_POINT('',(-0.00534029243944068,-0.00287504504673827,-0.00952544530782837));
#28653=CARTESIAN_POINT('',(-0.00594156053203977,-0.00121351369403066,-0.00945300176598398));
#28654=CARTESIAN_POINT('',(-0.00605668045273713,-0.000315825750337319,-0.00941678049889378));
#28655=CARTESIAN_POINT('',(-0.00588978902176606,0.00144337707403134,-0.00934433689106272));
#28656=CARTESIAN_POINT('',(-0.00560996798134601,0.00230387638883739,-0.0093081155893231));
#28657=CARTESIAN_POINT('',(-0.00470721006664119,0.00382310259118043,-0.00923567213389156));
#28658=CARTESIAN_POINT('',(-0.00408613400847974,0.00448099997245,-0.00919945065898276));
#28659=CARTESIAN_POINT('',(-0.0026207737514388,0.00546886741436465,-0.00912700747040132));
#28660=CARTESIAN_POINT('',(-0.00177786617410126,0.00579763556459996,-0.00909078577361959));
#28661=CARTESIAN_POINT('',(-3.09466222681958E-5,0.00606464167597443,-0.00901834285446272));
#28662=CARTESIAN_POINT('',(0.000871699766989816,0.00600111463142254,-0.00898212098023906));
#28663=CARTESIAN_POINT('',(0.00256503164149829,0.00549586755061753,-0.0089096782211661));
#28664=CARTESIAN_POINT('',(0.00335400980216468,0.00505238808937253,-0.00887345630384614));
#28665=CARTESIAN_POINT('',(0.00466851979026242,0.00387159456299146,-0.00880101349138235));
#28666=CARTESIAN_POINT('',(0.00519260976097037,0.0031334713015793,-0.00876479174579288));
#28667=CARTESIAN_POINT('',(0.00587523641665553,0.00150374624037253,-0.00869234857723131));
#28668=CARTESIAN_POINT('',(0.0060340189891069,0.000612553833172357,-0.00865612712601019));
#28669=CARTESIAN_POINT('',(0.00595367775238934,-0.00115259631367031,-0.00858368358416579));
#28670=CARTESIAN_POINT('',(0.0057165043874037,-0.00202600631780788,-0.00854746231707637));
#28671=CARTESIAN_POINT('',(0.00488909903514167,-0.00358743121515669,-0.00847501870924377));
#28672=CARTESIAN_POINT('',(0.00430127927179329,-0.00427534604365617,-0.00843879740750493));
#28673=CARTESIAN_POINT('',(0.00288585701391485,-0.00533345753983467,-0.00836635395207338));
#28674=CARTESIAN_POINT('',(0.0020602911276489,-0.00570359994720765,-0.00833013247716457));
#28675=CARTESIAN_POINT('',(0.000328434275016982,-0.00605550136479379,-0.00825768928858313));
#28676=CARTESIAN_POINT('',(-0.000576124907666656,-0.00603667676488749,-0.00822146759180141));
#28677=CARTESIAN_POINT('',(-0.00229224694171241,-0.00561484107607418,-0.00814902467264454));
#28678=CARTESIAN_POINT('',(-0.00310187271838032,-0.00521072192139484,-0.00811280279842165));
#28679=CARTESIAN_POINT('',(-0.004472957691924,-0.00409592443072183,-0.00804036003934715));
#28680=CARTESIAN_POINT('',(-0.00503216622374263,-0.00338427396279622,-0.00800413812202796));
#28681=CARTESIAN_POINT('',(-0.00579474497744008,-0.00179032179752817,-0.00793169530956417));
#28682=CARTESIAN_POINT('',(-0.00599647343138397,-0.000907824274979786,-0.00789547356397393));
#28683=CARTESIAN_POINT('',(-0.00600346944668562,0.000859075264311016,-0.00782303039541389));
#28684=CARTESIAN_POINT('',(-0.00580912084621274,0.0017431931486827,-0.00778680894419278));
#28685=CARTESIAN_POINT('',(-0.00505940150514794,0.00334323398092366,-0.00771436540234685));
#28686=CARTESIAN_POINT('',(-0.00450604234934851,0.00405939728987541,-0.00767814413525819));
#28687=CARTESIAN_POINT('',(-0.00314408804019073,0.00518533147390397,-0.00760570052742559));
#28688=CARTESIAN_POINT('',(-0.00233775978429126,0.00559593301943496,-0.00756947922568675));
#28689=CARTESIAN_POINT('',(-0.000625158391191966,0.00603184192596372,-0.00749703577025521));
#28690=CARTESIAN_POINT('',(0.000279212400785439,0.00605787853325739,-0.0074608142953487));
#28691=CARTESIAN_POINT('',(0.00201390634250682,0.0057202401256973,-0.00738837110676266));
#28692=CARTESIAN_POINT('',(0.00284240619482905,0.00535668865032929,-0.0073521494099817));
#28693=CARTESIAN_POINT('',(0.00426646668808612,0.00431023182100547,-0.0072797064908279));
#28694=CARTESIAN_POINT('',(0.00485981366694846,0.00362704403415547,-0.00724348461660347));
#28695=CARTESIAN_POINT('',(0.00569991648121184,0.00207241394588719,-0.00717104185752897));
#28696=CARTESIAN_POINT('',(0.00594422095445765,0.00120093480390459,-0.00713481994020902));
#28697=CARTESIAN_POINT('',(0.00603877277129507,-0.00056351123230199,-0.00706237712774675));
#28698=CARTESIAN_POINT('',(0.0058874283800451,-0.00145603076804085,-0.0070261553821569));
#28699=CARTESIAN_POINT('',(0.00521772867503515,-0.00309111034753677,-0.00695371221359457));
#28700=CARTESIAN_POINT('',(0.00469983671428812,-0.00383355477573512,-0.006917490762375));
#28701=CARTESIAN_POINT('',(0.00339487724234326,-0.00502489458107331,-0.00684504722052831));
#28702=CARTESIAN_POINT('',(0.00260957621096805,-0.00547478182307112,-0.00680882595343965));
#28703=CARTESIAN_POINT('',(0.00092041814236392,-0.00599381202091195,-0.00673638234560783));
#28704=CARTESIAN_POINT('',(1.83375614742641E-5,-0.00606458992025192,-0.00670016104386784));
#28705=CARTESIAN_POINT('',(-0.00173071492951204,-0.00581193305766056,-0.00662771758843784));
#28706=CARTESIAN_POINT('',(-0.00257620837226887,-0.00548990002742911,-0.00659149611352898));
#28707=CARTESIAN_POINT('',(-0.00404964797548944,-0.00451412418156432,-0.00651905292494602));
#28708=CARTESIAN_POINT('',(-0.00467595690530402,-0.00386119324726373,-0.00648283122816474));
#28709=CARTESIAN_POINT('',(-0.00559115555681467,-0.002349428843539,-0.00641038830900865));
#28710=CARTESIAN_POINT('',(-0.00587789203904983,-0.00149118157195279,-0.00637416643478492));
#28711=CARTESIAN_POINT('',(-0.00605911465610112,0.000266602775729709,-0.0063017236757112));
#28712=CARTESIAN_POINT('',(-0.0059513219293497,0.00116523579237788,-0.00626550175839094));
#28713=CARTESIAN_POINT('',(-0.00536345215233749,0.00283155478525354,-0.00619305894592869));
#28714=CARTESIAN_POINT('',(-0.0048820757275079,0.00359821832558035,-0.00615683720033756));
#28715=CARTESIAN_POINT('',(-0.00363763601144603,0.0048525519013342,-0.00608439403177752));
#28716=CARTESIAN_POINT('',(-0.00287504504674204,0.00534029243944514,-0.00604817258055424));
#28717=CARTESIAN_POINT('',(-0.00121351369403187,0.00594156053203358,-0.0059757290387129));
#28718=CARTESIAN_POINT('',(-0.00031582575033843,0.00605668045273254,-0.00593950777162106));
#28719=CARTESIAN_POINT('',(0.00144337707403289,0.00588978902177064,-0.00586706416378998));
#28720=CARTESIAN_POINT('',(0.00230387638884796,0.00560996798136351,-0.00583084286204893));
#28721=CARTESIAN_POINT('',(0.00382310259116669,0.00470721006662557,-0.00575839940662044));
#28722=CARTESIAN_POINT('',(0.00448099997245725,0.00408613400848599,-0.0057221779317101));
#28723=CARTESIAN_POINT('',(0.00546886741435594,0.00262077375143485,-0.00564973474312865));
#28724=CARTESIAN_POINT('',(0.00579763556459787,0.00177786617410278,-0.00561351304634461));
#28725=CARTESIAN_POINT('',(0.00606464167597621,3.0946622268693E-5,-0.00554107012719234));
#28726=CARTESIAN_POINT('',(0.00600111463141991,-0.000871699766989554,-0.0055048482529664));
#28727=CARTESIAN_POINT('',(0.00549586755062006,-0.00256503164149915,-0.0054324054938933));
#28728=CARTESIAN_POINT('',(0.00505238808936695,-0.00335400980216068,-0.00539618357657267));
#28729=CARTESIAN_POINT('',(0.00387159456299719,-0.00466851979026632,-0.00532374076411039));
#28730=CARTESIAN_POINT('',(0.00313347130158231,-0.00519260976097808,-0.00528751901851862));
#28731=CARTESIAN_POINT('',(0.00150374624036927,-0.00587523641664796,-0.00521507584996011));
#28732=CARTESIAN_POINT('',(0.000612553833171035,-0.00603401898911497,-0.00517885439873749));
#28733=CARTESIAN_POINT('',(-0.00115259631366817,-0.00595367775238131,-0.0051064108568931));
#28734=CARTESIAN_POINT('',(-0.00202600631781078,-0.00571650438740787,-0.00507018958980372));
#28735=CARTESIAN_POINT('',(-0.00358743121515375,-0.00488909903513752,-0.00499774598197099));
#28736=CARTESIAN_POINT('',(-0.00427534604366103,-0.00430127927179586,-0.00496152468023219));
#28737=CARTESIAN_POINT('',(-0.00533345753983033,-0.00288585701391166,-0.00488908122480065));
#28738=CARTESIAN_POINT('',(-0.00570359994720922,-0.00206029112764941,-0.00485285974989415));
#28739=CARTESIAN_POINT('',(-0.00605550136479229,-0.000328434275016135,-0.00478041656130811));
#28740=CARTESIAN_POINT('',(-0.00603667676488204,0.000576124907666373,-0.00474419486452637));
#28741=CARTESIAN_POINT('',(-0.00561484107607947,0.00229224694171347,-0.00467175194537411));
#28742=CARTESIAN_POINT('',(-0.00521072192140026,0.00310187271838521,-0.00463553007114899));
#28743=CARTESIAN_POINT('',(-0.00409592443071614,0.00447295769191944,-0.00456308731207436));
#28744=CARTESIAN_POINT('',(-0.00338427396279826,0.00503216622374612,-0.00452686539475448));
#28745=CARTESIAN_POINT('',(-0.00179032179752601,0.00579474497743666,-0.00445442258229221));
#28746=CARTESIAN_POINT('',(-0.000907824274979335,0.0059964734313974,-0.00441820083669967));
#28747=CARTESIAN_POINT('',(0.00085907526431096,0.00600346944667221,-0.0043457576681427));
#28748=CARTESIAN_POINT('',(0.00174319314868342,0.00580912084621372,-0.00430953621691928));
#28749=CARTESIAN_POINT('',(0.00334323398092361,0.00505940150514661,-0.00423709267507489));
#28750=CARTESIAN_POINT('',(0.00405939728986873,0.00450604234934388,-0.00420087140798552));
#28751=CARTESIAN_POINT('',(0.00518533147391094,0.00314408804019501,-0.00412842780015279));
#28752=CARTESIAN_POINT('',(0.00559593301943005,0.00233775978429005,-0.00409220649841479));
#28753=CARTESIAN_POINT('',(0.00603184192596878,0.000625158391192479,-0.00401976304298171));
#28754=CARTESIAN_POINT('',(0.00605787853326322,-0.000279212400785085,-0.00398354156807523));
#28755=CARTESIAN_POINT('',(0.00572024012569162,-0.00201390634250648,-0.00391109837949073));
#28756=CARTESIAN_POINT('',(0.00535668865032563,-0.00284240619482649,-0.0038748766827105));
#28757=CARTESIAN_POINT('',(0.00431023182100872,-0.0042664666880893,-0.00380243376355363));
#28758=CARTESIAN_POINT('',(0.00362704403415923,-0.00485981366695353,-0.00376621188933157));
#28759=CARTESIAN_POINT('',(0.00207241394588276,-0.00569991648120711,-0.0036937691302554));
#28760=CARTESIAN_POINT('',(0.00120093480390449,-0.00594422095445802,-0.00365754721293706));
#28761=CARTESIAN_POINT('',(-0.000563511232301889,-0.00603877277129467,-0.00358510440047326));
#28762=CARTESIAN_POINT('',(-0.00145603076803988,-0.00588742838004119,-0.00354888265488379));
#28763=CARTESIAN_POINT('',(-0.00309111034753821,-0.00521772867503886,-0.00347643948632222));
#28764=CARTESIAN_POINT('',(-0.00383355477573305,-0.00469983671428823,-0.00344021803510188));
#28765=CARTESIAN_POINT('',(-0.005024894581076,-0.00339487724234243,-0.00336777449325594));
#28766=CARTESIAN_POINT('',(-0.00547478182306962,-0.00260957621096737,-0.00333155322616581));
#28767=CARTESIAN_POINT('',(-0.00599381202091404,-0.000920418142362637,-0.00325910961833615));
#28768=CARTESIAN_POINT('',(-0.00606458992025173,-1.83375614733508E-5,-0.00322288831659661));
#28769=CARTESIAN_POINT('',(-0.00581193305766033,0.00173071492951357,-0.00315044486116353));
#28770=CARTESIAN_POINT('',(-0.00548990002742595,0.00257620837226724,-0.00311422338625548));
#28771=CARTESIAN_POINT('',(-0.00451412418156716,0.00404964797549147,-0.00304178019767404));
#28772=CARTESIAN_POINT('',(-0.00386119324726109,0.00467595690530463,-0.00300555850089079));
#28773=CARTESIAN_POINT('',(-0.00234942884353807,0.00559115555681618,-0.00293311558173699));
#28774=CARTESIAN_POINT('',(-0.00149118157195182,0.00587789203904661,-0.00289689370751264));
#28775=CARTESIAN_POINT('',(0.000266602775729427,0.0060591146561044,-0.00282445094843801));
#28776=CARTESIAN_POINT('',(0.00116523579237932,0.00595132192934975,-0.00278822903111813));
#28777=CARTESIAN_POINT('',(0.00283155478525638,0.00536345215233592,-0.00271578621865587));
#28778=CARTESIAN_POINT('',(0.00359821832558002,0.00488207572750747,-0.00267956447306408));
#28779=CARTESIAN_POINT('',(0.00485255190133472,0.00363763601144627,-0.00260712130450557));
#28780=CARTESIAN_POINT('',(0.00534029243944329,0.0028750450467383,-0.00257089985328367));
#28781=CARTESIAN_POINT('',(0.00594156053203786,0.00121351369402893,-0.00249845631143773));
#28782=CARTESIAN_POINT('',(0.00605668045272946,0.00031582575033894,-0.00246223504434917));
#28783=CARTESIAN_POINT('',(0.00588978902177369,-0.00144337707403387,-0.00238979143651642));
#28784=CARTESIAN_POINT('',(0.00560996798136092,-0.00230387638884949,-0.00235357013477837));
#28785=CARTESIAN_POINT('',(0.00470721006662452,-0.00382310259117127,-0.00228112667934528));
#28786=CARTESIAN_POINT('',(0.00408613400848635,-0.00448099997246406,-0.00224490520443801));
#28787=CARTESIAN_POINT('',(0.00262077375142909,-0.00546886741435278,-0.00217246201585504));
#28788=CARTESIAN_POINT('',(0.00177786617409953,-0.00579763556459878,-0.00213624031907329));
#28789=CARTESIAN_POINT('',(3.09466222649569E-5,-0.00606464167597636,-0.00206379739991795));
#28790=CARTESIAN_POINT('',(-0.000871699766989641,-0.00600111463142063,-0.00202757552569444));
#28791=CARTESIAN_POINT('',(-0.0025650316414994,-0.00549586755061925,-0.00195513276661981));
#28792=CARTESIAN_POINT('',(-0.00335400980216594,-0.0050523880893681,-0.00191891084930058));
#28793=CARTESIAN_POINT('',(-0.00466851979026617,-0.00387159456299146,-0.00184646803683676));
#28794=CARTESIAN_POINT('',(-0.00519260976097701,-0.00313347130158175,-0.0018102462912459));
#28795=CARTESIAN_POINT('',(-0.00587523641664912,-0.00150374624036962,-0.0017378031226874));
#28796=CARTESIAN_POINT('',(-0.00603401898911557,-0.00061255383316749,-0.00170158167146463));
#28797=CARTESIAN_POINT('',(-0.00595367775238039,0.00115259631367158,-0.00162913812962024));
#28798=CARTESIAN_POINT('',(-0.00571650438740898,0.00202600631781163,-0.00159291686253176));
#28799=CARTESIAN_POINT('',(-0.00488909903513646,0.00358743121515282,-0.00152047325469751));
#28800=CARTESIAN_POINT('',(-0.0043012792717929,0.0042753460436607,-0.00148425195295939));
#28801=CARTESIAN_POINT('',(-0.00288585701391163,0.00533345753983288,-0.00141180849752786));
#28802=CARTESIAN_POINT('',(-0.00206029112764908,0.00570359994721081,-0.00137558702261988));
#28803=CARTESIAN_POINT('',(-0.000328434275016096,0.00605550136479076,-0.00130314383403692));
#28804=CARTESIAN_POINT('',(0.000576124907667665,0.00603667676488167,-0.00126692213725589));
#28805=CARTESIAN_POINT('',(0.00229224694171486,0.00561484107607917,-0.00119447921809904));
#28806=CARTESIAN_POINT('',(0.00310187271838672,0.00521072192140026,-0.00115825734387622));
#28807=CARTESIAN_POINT('',(0.00447295769191957,0.00409592443071479,-0.00108581458480161));
#28808=CARTESIAN_POINT('',(0.00503216622374031,0.00338427396279337,-0.00104959266748173));
#28809=CARTESIAN_POINT('',(0.005794744977443,0.0017903217975298,-0.000977149855019475));
#28810=CARTESIAN_POINT('',(0.00599647343139357,0.000907824274979128,-0.000940928109428471));
#28811=CARTESIAN_POINT('',(0.00600346944667604,-0.000859075264311266,-0.000868484940868442));
#28812=CARTESIAN_POINT('',(0.00580912084621264,-0.0017431931486827,-0.0008322634896458));
#28813=CARTESIAN_POINT('',(0.00505940150514784,-0.00334323398092403,-0.000759819947802938));
#28814=CARTESIAN_POINT('',(0.00450604234934318,-0.00405939728986845,-0.000723598680712034));
#28815=CARTESIAN_POINT('',(0.00314408804019546,-0.00518533147391142,-0.000651155072880834));
#28816=CARTESIAN_POINT('',(0.00233775978428977,-0.00559593301942972,-0.000614933771140532));
#28817=CARTESIAN_POINT('',(0.000625158391192401,-0.00603184192596921,-0.000542490315710523));
#28818=CARTESIAN_POINT('',(-0.000279212400785806,-0.00605787853326039,-0.000506268840800958));
#28819=CARTESIAN_POINT('',(-0.00201390634250717,-0.00572024012569417,-0.000433825652219523));
#28820=CARTESIAN_POINT('',(-0.00284240619482663,-0.00535668865032544,-0.000397603955437035));
#28821=CARTESIAN_POINT('',(-0.00426646668808866,-0.0043102318210093,-0.000325161036281701));
#28822=CARTESIAN_POINT('',(-0.00485981366695287,-0.00362704403415734,-0.000288939162058086));
#28823=CARTESIAN_POINT('',(-0.00569991648120799,-0.00207241394588432,-0.000216496402983457));
#28824=CARTESIAN_POINT('',(-0.0059442209544565,-0.00120093480390377,-0.000180274485662048));
#28825=CARTESIAN_POINT('',(-0.00603877277129622,0.000563511232301556,-0.000107831673202851));
#28826=CARTESIAN_POINT('',(-0.00588742838004495,0.00145603076804102,-7.16099276087707E-5));
#28827=CARTESIAN_POINT('',(-0.00521772867503495,0.00309111034753743,8.33240948196383E-7));
#28828=CARTESIAN_POINT('',(-0.00469983671428809,0.00383355477573433,3.70546921731411E-5));
#28829=CARTESIAN_POINT('',(-0.00339487724234229,0.00502489458107499,0.000109498234014469));
#28830=CARTESIAN_POINT('',(-0.00260957621096751,0.00547478182307082,0.000145719501104603));
#28831=CARTESIAN_POINT('',(-0.000920418142362202,0.00599381202091294,0.000218163108938871));
#28832=CARTESIAN_POINT('',(-1.83375614725771E-5,0.00606458992025286,0.00025438441067611));
#28833=CARTESIAN_POINT('',(0.00173071492951319,0.00581193305765916,0.000326827866109187));
#28834=CARTESIAN_POINT('',(0.00257620837226795,0.00548990002742626,0.000363049341015702));
#28835=CARTESIAN_POINT('',(0.00404964797549103,0.0045141241815667,0.000435492529600207));
#28836=CARTESIAN_POINT('',(0.00467595690530011,0.00386119324726,0.000471714226381924));
#28837=CARTESIAN_POINT('',(0.00559115555682087,0.00234942884353889,0.000544157145535723));
#28838=CARTESIAN_POINT('',(0.00587789203904666,0.00149118157195146,0.000580379019759321));
#28839=CARTESIAN_POINT('',(0.00605911465610445,-0.000266602775729979,0.000652821778835484));
#28840=CARTESIAN_POINT('',(0.00595132192935104,-0.0011652357923806,0.000689043696154603));
#28841=CARTESIAN_POINT('',(0.00536345215233414,-0.0028315547852565,0.000761486508616866));
#28842=CARTESIAN_POINT('',(0.00488207572750542,-0.00359821832557824,0.000797708254208643));
#28843=CARTESIAN_POINT('',(0.00363763601144815,-0.00485255190133669,0.000870151422767143));
#28844=CARTESIAN_POINT('',(0.0028750450467372,-0.00534029243944135,0.000906372873988264));
#28845=CARTESIAN_POINT('',(0.00121351369403036,-0.00594156053203968,0.000978816415835729));
#28846=CARTESIAN_POINT('',(0.000315825750338376,-0.00605668045273214,0.00101503768292201));
#28847=CARTESIAN_POINT('',(-0.0014433770740335,-0.00588978902177103,0.00108748129075781));
#28848=CARTESIAN_POINT('',(-0.0023038763888485,-0.00560996798135989,0.00112370259249429));
#28849=CARTESIAN_POINT('',(-0.00382310259117005,-0.0047072100666267,0.00119614604792737));
#28850=CARTESIAN_POINT('',(-0.00448099997246035,-0.00408613400848585,0.00123236752283539));
#28851=CARTESIAN_POINT('',(-0.00546886741435506,-0.00262077375143265,0.00130481071141683));
#28852=CARTESIAN_POINT('',(-0.00579763556459847,-0.0017778661740996,0.00134103240820018));
#28853=CARTESIAN_POINT('',(-0.00606464167597601,-3.09466222654928E-5,0.00141347532735398));
#28854=CARTESIAN_POINT('',(-0.00600111463141992,0.000871699766980109,0.00144969720157956));
#28855=CARTESIAN_POINT('',(-0.00549586755062015,0.00256503164149748,0.00152213996065112));
#28856=CARTESIAN_POINT('',(-0.00505238808936944,0.00335400980220972,0.00155836187797583));
#28857=CARTESIAN_POINT('',(-0.00387159456298909,0.00466851979024306,0.00163080469043323));
#28858=CARTESIAN_POINT('',(-0.00313347130160139,0.00519260976081515,0.00166702643602028));
#28859=CARTESIAN_POINT('',(-0.00150374624037983,0.00587523641686614,0.00173946960459158));
#28860=CARTESIAN_POINT('',(-0.000612553833165579,0.00603401898939451,0.00177569105583878));
#28861=CARTESIAN_POINT('',(0.00115259631371467,0.0059536777513449,0.00184813459759908));
#28862=CARTESIAN_POINT('',(0.00202600631845691,0.00571650438746742,0.00188435586467389));
#28863=CARTESIAN_POINT('',(0.00358743121405334,0.00488909903965777,0.00195679947282889));
#28864=CARTESIAN_POINT('',(0.00427534604012664,0.00430127926719982,0.0019930207743065));
#28865=CARTESIAN_POINT('',(0.00533345754995747,0.00288585699514267,0.00206546422868242));
#28866=CARTESIAN_POINT('',(0.00570359995483104,0.0020602911659135,0.00210168570590789));
#28867=CARTESIAN_POINT('',(0.00605550130478085,0.000328434353748034,0.00217412889706531));
#28868=CARTESIAN_POINT('',(0.00603667678110669,-0.000576125165779344,0.00221035058020653));
#28869=CARTESIAN_POINT('',(0.0056148413322424,-0.00229224724916889,0.00228279349810771));
#28870=CARTESIAN_POINT('',(0.00521072173073282,-0.00310187120641182,0.00231901543922011));
#28871=CARTESIAN_POINT('',(0.00409592363987556,-0.00447295679573389,0.00239145815903209));
#28872=CARTESIAN_POINT('',(0.00338427466196768,-0.00503217385805823,0.00242767978760003));
#28873=CARTESIAN_POINT('',(0.00179032336308774,-0.00579474532206606,0.00250012295961856));
#28874=CARTESIAN_POINT('',(0.000907823357868306,-0.00599643245723689,0.00253634580897236));
#28875=CARTESIAN_POINT('',(-0.00154620346649854,-0.00600624349949343,0.00263695810271456));
#28876=CARTESIAN_POINT('',(-0.00311036825890238,-0.00536525626263524,0.00270138359384264));
#28877=CARTESIAN_POINT('',(-0.00534036428216497,-0.00315440800084661,0.00283011272614596));
#28878=CARTESIAN_POINT('',(-0.005993747924043,-0.00158510314530943,0.00289494802175126));
#28879=CARTESIAN_POINT('',(-0.00599994287806968,-2.43712307521179E-5,0.00295892997067846));
#28880=CARTESIAN_POINT('',(-0.00481,-2.43712308653838E-5,-0.0140410700265819));
#28881=CARTESIAN_POINT('',(-0.00481309747552789,0.0005972081498295,-0.0140093885644531));
#28882=CARTESIAN_POINT('',(-0.00468998407530162,0.00123726682455829,-0.0139764807930202));
#28883=CARTESIAN_POINT('',(-0.00391925933224434,0.00312747621252669,-0.013872784228301));
#28884=CARTESIAN_POINT('',(-0.0027740912685582,0.00417781018427425,-0.0137998290452317));
#28885=CARTESIAN_POINT('',(-0.000743052669427504,0.00480421623630904,-0.0136910345094936));
#28886=CARTESIAN_POINT('',(-2.09107523793298E-5,0.00486189283259464,-0.0136549080475063));
#28887=CARTESIAN_POINT('',(0.00138336308198147,0.00466047772833265,-0.0135822476417793));
#28888=CARTESIAN_POINT('',(0.00205983412778109,0.00440373135422188,-0.0135462440918831));
#28889=CARTESIAN_POINT('',(0.00324376540199818,0.00362139882094577,-0.0134735141781805));
#28890=CARTESIAN_POINT('',(0.00374510470485854,0.00309961711105746,-0.013437502604144));
#28891=CARTESIAN_POINT('',(0.00448098642623155,0.00188681812047127,-0.0133648332519321));
#28892=CARTESIAN_POINT('',(0.00471091204467595,0.00119985910905067,-0.0133287331669378));
#28893=CARTESIAN_POINT('',(0.00485766819906913,-0.000209707601454214,-0.013256221775084));
#28894=CARTESIAN_POINT('',(0.00477148103078713,-0.000930579595599502,-0.0132199460668666));
#28895=CARTESIAN_POINT('',(0.00430207967528991,-0.00226535979212377,-0.0131476977203435));
#28896=CARTESIAN_POINT('',(0.00391509509971101,-0.00288228528512647,-0.0131111635028226));
#28897=CARTESIAN_POINT('',(0.00292169918444729,-0.00388557413442109,-0.0130392727679438));
#28898=CARTESIAN_POINT('',(0.00230884595336562,-0.00427892221022316,-0.013002738946633));
#28899=CARTESIAN_POINT('',(0.000978852813182588,-0.00476172053905318,-0.0129304897411354));
#28900=CARTESIAN_POINT('',(0.000258925775658046,-0.00485523411194574,-0.0128942145009195));
#28901=CARTESIAN_POINT('',(-0.00115205885285439,-0.00472280803267504,-0.0128217027604969));
#28902=CARTESIAN_POINT('',(-0.00184127085788122,-0.00449979694527318,-0.0127856034436556));
#28903=CARTESIAN_POINT('',(-0.003061531144935,-0.00377635423162404,-0.0127129318637898));
#28904=CARTESIAN_POINT('',(-0.0035882725709729,-0.00328025220172361,-0.0126769213982539));
#28905=CARTESIAN_POINT('',(-0.00438269974044985,-0.0021043945145923,-0.0126041963336704));
#28906=CARTESIAN_POINT('',(-0.00464619750861001,-0.00143048448148469,-0.012568185646273));
#28907=CARTESIAN_POINT('',(-0.00486194590083409,-2.83941718657882E-5,-0.0124955146026973));
#28908=CARTESIAN_POINT('',(-0.00481148142262297,0.000694263094901001,-0.0124594147133711));
#28909=CARTESIAN_POINT('',(-0.00440764851959399,0.0020526935874246,-0.0123869038211612));
#28910=CARTESIAN_POINT('',(-0.00405215626122202,0.0026857101246237,-0.0123506279316278));
#28911=CARTESIAN_POINT('',(-0.00310768769660497,0.00373925423709306,-0.0122783794579231));
#28912=CARTESIAN_POINT('',(-0.00251407341947778,0.00416112641085721,-0.0122418453259864));
#28913=CARTESIAN_POINT('',(-0.00121235323067996,0.00470788827290766,-0.0121699545995431));
#28914=CARTESIAN_POINT('',(-0.000495622876170741,0.00483676574590065,-0.0121334207619492));
#28915=CARTESIAN_POINT('',(0.000917889479731042,0.00477384690220689,-0.0120611715589283));
#28916=CARTESIAN_POINT('',(0.00161880142913311,0.00458473802635917,-0.0120248963195875));
#28917=CARTESIAN_POINT('',(0.00287170398311334,0.0039224318405235,-0.0119523845786562));
#28918=CARTESIAN_POINT('',(0.00342311019952517,0.00345264644636138,-0.0119162852617685));
#28919=CARTESIAN_POINT('',(0.00427363416207398,0.00231729913548141,-0.0118436136819951));
#28920=CARTESIAN_POINT('',(0.00457042975696389,0.00165738540690319,-0.011807603216425));
#28921=CARTESIAN_POINT('',(0.00485440350323103,0.000267020440622511,-0.0117348781518639));
#28922=CARTESIAN_POINT('',(0.00483994949353749,-0.000456427476013854,-0.0116988674644479));
#28923=CARTESIAN_POINT('',(0.00450271828510177,-0.001834353351076,-0.0116261964208863));
#28924=CARTESIAN_POINT('',(0.00417954622328539,-0.00248268968912301,-0.0115900965315827));
#28925=CARTESIAN_POINT('',(0.00328660442614019,-0.00358317565608095,-0.0115175856393133));
#28926=CARTESIAN_POINT('',(0.00271592746345113,-0.00403196568092759,-0.0114813097498018));
#28927=CARTESIAN_POINT('',(0.00144017841039003,-0.00464388105095874,-0.0114090612761124));
#28928=CARTESIAN_POINT('',(0.000730306838075062,-0.00480647376857319,-0.0113725271441584));
#28929=CARTESIAN_POINT('',(-0.000681562507468831,-0.00481346911223833,-0.0113006364177347));
#28930=CARTESIAN_POINT('',(-0.00139305428604887,-0.00465825553959685,-0.0112641025801363));
#28931=CARTESIAN_POINT('',(-0.00267489142155627,-0.00405919834765848,-0.0111918533771047));
#28932=CARTESIAN_POINT('',(-0.00325008079200792,-0.00361625713726751,-0.0111555781377456));
#28933=CARTESIAN_POINT('',(-0.00415415821336922,-0.00252490095812974,-0.0110830663968616));
#28934=CARTESIAN_POINT('',(-0.00448381204370197,-0.00187986182427054,-0.011046967079966));
#28935=CARTESIAN_POINT('',(-0.00483511511877081,-0.000505456252163206,-0.0109742955001612));
#28936=CARTESIAN_POINT('',(-0.00485678044348491,0.000217803291852025,-0.0109382850346499));
#28937=CARTESIAN_POINT('',(-0.00458706833793583,0.00161100507485156,-0.0108655599700028));
#28938=CARTESIAN_POINT('',(-0.00429686304231609,0.00227385248782169,-0.0108295492826413));
#28939=CARTESIAN_POINT('',(-0.00345799262771523,0.00341783720477129,-0.0107568782390567));
#28940=CARTESIAN_POINT('',(-0.00291131299915783,0.00389314928382754,-0.0107207783497292));
#28941=CARTESIAN_POINT('',(-0.00166520460192398,0.0045681517126536,-0.0106482674575304));
#28942=CARTESIAN_POINT('',(-0.000966223329313709,0.004764391012167,-0.0106119915679807));
#28943=CARTESIAN_POINT('',(0.000446584983549955,0.00484151907170173,-0.0105397430942975));
#28944=CARTESIAN_POINT('',(0.00116464233918176,0.00472007906581758,-0.0105032089623268));
#28945=CARTESIAN_POINT('',(0.00247171653223062,0.00418624291343643,-0.01043131823593));
#28946=CARTESIAN_POINT('',(0.0030696515612859,0.00377056815459063,-0.0103947843983099));
#28947=CARTESIAN_POINT('',(0.00402466539239388,0.00272657364139763,-0.0103225351952951));
#28948=CARTESIAN_POINT('',(0.00438656481634017,0.00209723388046881,-0.0102862599559436));
#28949=CARTESIAN_POINT('',(0.00480417951319281,0.000742976793155331,-0.0102137482150274));
#28950=CARTESIAN_POINT('',(0.0048618941500755,2.0885280433355E-5,-0.0101776488981767));
#28951=CARTESIAN_POINT('',(0.00466049362906918,-0.00138333776357924,-0.0101049773183144));
#28952=CARTESIAN_POINT('',(0.00440373033433314,-0.00205983341381495,-0.010068966852824));
#28953=CARTESIAN_POINT('',(0.00362139360004503,-0.0032437696714788,-0.00999624178819235));
#28954=CARTESIAN_POINT('',(0.00309961814406215,-0.00374510407087602,-0.00996023110084268));
#28955=CARTESIAN_POINT('',(0.00188681893954217,-0.00448098632681852,-0.009887560057219));
#28956=CARTESIAN_POINT('',(0.00119985876200896,-0.00471091219153308,-0.00985146016793407));
#28957=CARTESIAN_POINT('',(-0.000209707527798131,-0.00485766808139427,-0.00977894927568926));
#28958=CARTESIAN_POINT('',(-0.000930579547875865,-0.00477148100111361,-0.00974267338616599));
#28959=CARTESIAN_POINT('',(-0.00226535986204974,-0.00430207970226204,-0.00967042491247586));
#28960=CARTESIAN_POINT('',(-0.00288228527781962,-0.00391509511292238,-0.00963389078046685));
#28961=CARTESIAN_POINT('',(-0.00388557412111365,-0.00292169917944251,-0.00956200005415361));
#28962=CARTESIAN_POINT('',(-0.00427892221277846,-0.00230884594832664,-0.00952546621648906));
#28963=CARTESIAN_POINT('',(-0.00476172054092556,-0.000978852814690387,-0.00945321701347969));
#28964=CARTESIAN_POINT('',(-0.00485523411171129,-0.000258925776843735,-0.00941694177410321));
#28965=CARTESIAN_POINT('',(-0.0047228080321108,0.00115205885347806,-0.00934443003323146));
#28966=CARTESIAN_POINT('',(-0.00449979694528425,0.00184127085801928,-0.00930833071637539));
#28967=CARTESIAN_POINT('',(-0.00377635423181849,0.00306153114481296,-0.00923565913647926));
#28968=CARTESIAN_POINT('',(-0.00328025220168744,0.00358827257095472,-0.00919964867101474));
#28969=CARTESIAN_POINT('',(-0.00210439451456859,0.00438269974047501,-0.00912692360636535));
#28970=CARTESIAN_POINT('',(-0.00143048448149271,0.00464619750860692,-0.0090909129190107));
#28971=CARTESIAN_POINT('',(-2.83941718690916E-5,0.00486194590083703,-0.00901824187541456));
#28972=CARTESIAN_POINT('',(0.000694263094903329,0.00481148142262362,-0.00898214198609713));
#28973=CARTESIAN_POINT('',(0.00205269358742323,0.00440764851959351,-0.00890963109388991));
#28974=CARTESIAN_POINT('',(0.00268571012462705,0.00405215626122519,-0.00887335520434781));
#28975=CARTESIAN_POINT('',(0.00373925423709026,0.00310768769660104,-0.00880110673065769));
#28976=CARTESIAN_POINT('',(0.00416112641086552,0.0025140734194825,-0.00876457259869544));
#28977=CARTESIAN_POINT('',(0.00470788827289936,0.00121235323067521,-0.00869268187228864));
#28978=CARTESIAN_POINT('',(0.00483676574589448,0.000495622876171375,-0.00865614803468577));
#28979=CARTESIAN_POINT('',(0.00477384690221301,-0.00091788947973133,-0.00858389883164647));
#28980=CARTESIAN_POINT('',(0.00458473802636119,-0.00161880142913334,-0.00854762359231106));
#28981=CARTESIAN_POINT('',(0.00392243184052137,-0.00287170398311328,-0.00847511185138717));
#28982=CARTESIAN_POINT('',(0.00345264644635509,-0.00342311019951396,-0.00843901253452423));
#28983=CARTESIAN_POINT('',(0.00231729913548905,-0.00427363416208414,-0.00836634095469408));
#28984=CARTESIAN_POINT('',(0.00165738540690343,-0.00457042975695016,-0.00833033048917846));
#28985=CARTESIAN_POINT('',(0.000267020440624387,-0.00485440350324432,-0.00825760542456511));
#28986=CARTESIAN_POINT('',(-0.00045642747601189,-0.00483994949353287,-0.00822159473718368));
#28987=CARTESIAN_POINT('',(-0.00183435335107504,-0.00450271828510711,-0.00814892369360519));
#28988=CARTESIAN_POINT('',(-0.00248268968912489,-0.00417954622329111,-0.00811282380429882));
#28989=CARTESIAN_POINT('',(-0.00358317565607922,-0.00328660442613433,-0.0080403129120517));
#28990=CARTESIAN_POINT('',(-0.00403196568092499,-0.00271592746345426,-0.00800403702252997));
#28991=CARTESIAN_POINT('',(-0.0046438810509595,-0.00144017841039065,-0.00793178854883908));
#28992=CARTESIAN_POINT('',(-0.00480647376857799,-0.000730306838074603,-0.00789525441687993));
#28993=CARTESIAN_POINT('',(-0.00481346911223356,0.000681562507468902,-0.00782336369046775));
#28994=CARTESIAN_POINT('',(-0.00465825553960144,0.00139305428604982,-0.00778682985285337));
#28995=CARTESIAN_POINT('',(-0.00405919834765568,0.00267489142155148,-0.00771458064984247));
#28996=CARTESIAN_POINT('',(-0.00361625713727038,0.00325008079201076,-0.00767830541046259));
#28997=CARTESIAN_POINT('',(-0.0025249009581265,0.00415415821336665,-0.00760579366959928));
#28998=CARTESIAN_POINT('',(-0.00187986182427326,0.00448381204370238,-0.00756969435269181));
#28999=CARTESIAN_POINT('',(-0.000505456252163881,0.00483511511876958,-0.00749702277289005));
#29000=CARTESIAN_POINT('',(0.000217803291852552,0.00485678044349205,-0.00746101230736261));
#29001=CARTESIAN_POINT('',(0.00161100507485096,0.00458706833792869,-0.00738828724274465));
#29002=CARTESIAN_POINT('',(0.00227385248782256,0.00429686304231747,-0.00735227655536401));
#29003=CARTESIAN_POINT('',(0.00341783720476902,0.00345799262771487,-0.00727960551178858));
#29004=CARTESIAN_POINT('',(0.00389314928381935,0.00291131299915153,-0.0072435056224768));
#29005=CARTESIAN_POINT('',(0.00456815171266123,0.0016652046019313,-0.00717099473023737));
#29006=CARTESIAN_POINT('',(0.00476439101216452,0.000966223329314663,-0.00713471884071138));
#29007=CARTESIAN_POINT('',(0.00484151907170424,-0.000446584983550539,-0.00706247036702125));
#29008=CARTESIAN_POINT('',(0.00472007906582122,-0.00116464233918382,-0.00702593623504599));
#29009=CARTESIAN_POINT('',(0.0041862429134328,-0.00247171653222866,-0.00695404550866527));
#29010=CARTESIAN_POINT('',(0.00377056815458991,-0.00306965156128732,-0.00691751167103557));
#29011=CARTESIAN_POINT('',(0.00272657364139859,-0.00402466539239229,-0.00684526246802392));
#29012=CARTESIAN_POINT('',(0.00209723388046954,-0.00438656481634525,-0.006808987228659));
#29013=CARTESIAN_POINT('',(0.000742976793155499,-0.00480417951318747,-0.00673647548776654));
#29014=CARTESIAN_POINT('',(2.08852804327653E-5,-0.00486189415008334,-0.00670037617088551));
#29015=CARTESIAN_POINT('',(-0.0013833377635771,-0.0046604936290617,-0.00662770459105998));
#29016=CARTESIAN_POINT('',(-0.00205983341381761,-0.00440373033434133,-0.0065916941255317));
#29017=CARTESIAN_POINT('',(-0.00324376967147653,-0.00362139360003666,-0.00651896906093908));
#29018=CARTESIAN_POINT('',(-0.00374510407088497,-0.00309961814407148,-0.00648295837354621));
#29019=CARTESIAN_POINT('',(-0.00448098632680823,-0.00188681893953521,-0.00641028732997003));
#29020=CARTESIAN_POINT('',(-0.00471091219154346,-0.00119985876201278,-0.00637418744064019));
#29021=CARTESIAN_POINT('',(-0.00485766808138392,0.000209707527801528,-0.00630167654843758));
#29022=CARTESIAN_POINT('',(-0.00477148100110948,0.000930579547873459,-0.00626540065889905));
#29023=CARTESIAN_POINT('',(-0.00430207970226759,0.00226535986204828,-0.00619315218519742));
#29024=CARTESIAN_POINT('',(-0.00391509511291251,0.00288228527781205,-0.00615661805322093));
#29025=CARTESIAN_POINT('',(-0.00292169917945201,0.00388557412112162,-0.00608472732685399));
#29026=CARTESIAN_POINT('',(-0.00230884594833033,0.00427892221278309,-0.00604819348920526));
#29027=CARTESIAN_POINT('',(-0.000978852814690703,0.00476172054091953,-0.00597594428621812));
#29028=CARTESIAN_POINT('',(-0.000258925776844936,0.00485523411170668,-0.00593966904683851));
#29029=CARTESIAN_POINT('',(0.00115205885347961,0.00472280803211538,-0.00586715730595063));
#29030=CARTESIAN_POINT('',(0.00184127085802903,0.00449979694530251,-0.00583105798905901));
#29031=CARTESIAN_POINT('',(0.00306153114480066,0.00377635423180173,-0.00575838640925034));
#29032=CARTESIAN_POINT('',(0.00358827257096136,0.00328025220169526,-0.00572237594372284));
#29033=CARTESIAN_POINT('',(0.00438269974046719,0.00210439451456262,-0.00564965087911179));
#29034=CARTESIAN_POINT('',(0.00464619750860448,0.00143048448149637,-0.00561364019173723));
#29035=CARTESIAN_POINT('',(0.00486194590083922,2.83941718670394E-5,-0.00554096914814263));
#29036=CARTESIAN_POINT('',(0.00481148142262117,-0.000694263094902669,-0.00550486925883093));
#29037=CARTESIAN_POINT('',(0.00440764851959588,-0.00205269358742436,-0.00543235836661051));
#29038=CARTESIAN_POINT('',(0.00405215626121919,-0.00268571012462328,-0.00539608247708809));
#29039=CARTESIAN_POINT('',(0.00310768769660717,-0.00373925423709395,-0.00532383400337187));
#29040=CARTESIAN_POINT('',(0.0025140734194861,-0.00416112641087264,-0.00528729987140581));
#29041=CARTESIAN_POINT('',(0.00121235323067142,-0.00470788827289234,-0.00521540914503274));
#29042=CARTESIAN_POINT('',(0.000495622876171233,-0.00483676574590275,-0.00517887530739772));
#29043=CARTESIAN_POINT('',(-0.000917889479730532,-0.00477384690220479,-0.00510662610438912));
#29044=CARTESIAN_POINT('',(-0.00161880142913644,-0.00458473802636499,-0.00507035086502769));
#29045=CARTESIAN_POINT('',(-0.00287170398311014,-0.00392243184051759,-0.00499783912412512));
#29046=CARTESIAN_POINT('',(-0.0034231101995181,-0.00345264644635782,-0.00496173980723916));
#29047=CARTESIAN_POINT('',(-0.00427363416208043,-0.00231729913548583,-0.00488906822743356));
#29048=CARTESIAN_POINT('',(-0.0045704297569521,-0.00165738540690207,-0.00485305776190536));
#29049=CARTESIAN_POINT('',(-0.00485440350324243,-0.000267020440625468,-0.00478033269729277));
#29050=CARTESIAN_POINT('',(-0.00483994949352744,0.000456427476012682,-0.004744322009919));
#29051=CARTESIAN_POINT('',(-0.00450271828511242,0.00183435335107489,-0.0046716509663244));
#29052=CARTESIAN_POINT('',(-0.00417954622329755,0.00248268968912865,-0.00463555107701158));
#29053=CARTESIAN_POINT('',(-0.00328660442612768,0.00358317565607573,-0.00456304018479348));
#29054=CARTESIAN_POINT('',(-0.00271592746345708,0.00403196568092808,-0.0045267642952492));
#29055=CARTESIAN_POINT('',(-0.00144017841038773,0.00464388105095646,-0.00445451582157441));
#29056=CARTESIAN_POINT('',(-0.000730306838075307,0.00480647376858355,-0.00441798168957843));
#29057=CARTESIAN_POINT('',(0.000681562507469923,0.004813469112228,-0.00434609096322378));
#29058=CARTESIAN_POINT('',(0.00139305428604971,0.00465825553960303,-0.00430955712557991));
#29059=CARTESIAN_POINT('',(0.00267489142155213,0.00405919834765383,-0.00423730792257054));
#29060=CARTESIAN_POINT('',(0.0032500807920042,0.00361625713726574,-0.00420103268320758));
#29061=CARTESIAN_POINT('',(0.00415415821337343,0.00252490095813086,-0.00412852094230885));
#29062=CARTESIAN_POINT('',(0.00448381204369767,0.00187986182427097,-0.00409242162542985));
#29063=CARTESIAN_POINT('',(0.00483511511877444,0.000505456252165615,-0.0040197500456066));
#29064=CARTESIAN_POINT('',(0.00485678044349787,-0.000217803291852029,-0.00398373958007876));
#29065=CARTESIAN_POINT('',(0.00458706833792301,-0.00161100507485092,-0.00391101451548305));
#29066=CARTESIAN_POINT('',(0.00429686304231271,-0.00227385248782118,-0.00387500382810275));
#29067=CARTESIAN_POINT('',(0.00345799262771932,-0.0034178372047709,-0.00380233278450431));
#29068=CARTESIAN_POINT('',(0.00291131299915669,-0.00389314928382361,-0.00376623289519071));
#29069=CARTESIAN_POINT('',(0.00166520460192559,-0.00456815171265726,-0.00369372200297799));
#29070=CARTESIAN_POINT('',(0.000966223329313892,-0.00476439101216487,-0.00365744611343869));
#29071=CARTESIAN_POINT('',(-0.000446584983549747,-0.00484151907170383,-0.00358519763974856));
#29072=CARTESIAN_POINT('',(-0.0011646423391832,-0.00472007906581732,-0.0035486635077798));
#29073=CARTESIAN_POINT('',(-0.00247171653222966,-0.00418624291343652,-0.00347677278138603));
#29074=CARTESIAN_POINT('',(-0.00306965156128558,-0.00377056815458988,-0.0034402389437644));
#29075=CARTESIAN_POINT('',(-0.00402466539239451,-0.00272657364139803,-0.00336798974074966));
#29076=CARTESIAN_POINT('',(-0.00438656481634332,-0.00209723388046953,-0.003331714501389));
#29077=CARTESIAN_POINT('',(-0.00480417951318985,-0.000742976793153918,-0.00325920276049104));
#29078=CARTESIAN_POINT('',(-0.00486189415008336,-2.08852804317659E-5,-0.00322310344361396));
#29079=CARTESIAN_POINT('',(-0.00466049362906131,0.00138333776357806,-0.00315043186378611));
#29080=CARTESIAN_POINT('',(-0.00440373033433799,0.00205983341381625,-0.00311442139826632));
#29081=CARTESIAN_POINT('',(-0.00362139360003972,0.0032437696714782,-0.00304169633365911));
#29082=CARTESIAN_POINT('',(-0.00309961814406801,0.00374510407088595,-0.00300568564627766));
#29083=CARTESIAN_POINT('',(-0.00188681893953579,0.00448098632680893,-0.00293301460269303));
#29084=CARTESIAN_POINT('',(-0.00119985876201082,0.00471091219154023,-0.00289691471337792));
#29085=CARTESIAN_POINT('',(0.000209707527800109,0.00485766808138716,-0.00282440382115445));
#29086=CARTESIAN_POINT('',(0.000930579547875407,0.00477148100110929,-0.00278812793162741));
#29087=CARTESIAN_POINT('',(0.00226535986204975,0.00430207970226656,-0.00271587945792348));
#29088=CARTESIAN_POINT('',(0.0028822852778121,0.0039150951129117,-0.00267934532594897));
#29089=CARTESIAN_POINT('',(0.00388557412112173,0.00292169917945267,-0.0026074545995805));
#29090=CARTESIAN_POINT('',(0.00427892221278101,0.00230884594832717,-0.00257092076193929));
#29091=CARTESIAN_POINT('',(0.00476172054092358,0.000978852814688521,-0.00249867155893835));
#29092=CARTESIAN_POINT('',(0.00485523411170341,0.000258925776843461,-0.00246239631957351));
#29093=CARTESIAN_POINT('',(0.00472280803211865,-0.00115205885347851,-0.00238988457867017));
#29094=CARTESIAN_POINT('',(0.00449979694530029,-0.00184127085803015,-0.00235378526179305));
#29095=CARTESIAN_POINT('',(0.00377635423180104,-0.00306153114480446,-0.00228111368197056));
#29096=CARTESIAN_POINT('',(0.00328025220169769,-0.00358827257096685,-0.00224510321644117));
#29097=CARTESIAN_POINT('',(0.00210439451455585,-0.00438269974046463,-0.00217237815184775));
#29098=CARTESIAN_POINT('',(0.00143048448149287,-0.00464619750860529,-0.00213636746446399));
#29099=CARTESIAN_POINT('',(2.83941718649254E-5,-0.00486194590083927,-0.00206369642087015));
#29100=CARTESIAN_POINT('',(-0.000694263094903681,-0.00481148142262189,-0.00202759653155857));
#29101=CARTESIAN_POINT('',(-0.00205269358742362,-0.00440764851959508,-0.0019550856393374));
#29102=CARTESIAN_POINT('',(-0.00268571012462754,-0.00405215626122127,-0.00191880974980833));
#29103=CARTESIAN_POINT('',(-0.00373925423709378,-0.00310768769660141,-0.00184656127610592));
#29104=CARTESIAN_POINT('',(-0.00416112641087175,-0.00251407341948451,-0.00181002714413654));
#29105=CARTESIAN_POINT('',(-0.00470788827289332,-0.00121235323067282,-0.00173813641775658));
#29106=CARTESIAN_POINT('',(-0.0048367657459032,-0.000495622876167294,-0.00170160258012523));
#29107=CARTESIAN_POINT('',(-0.0047738469022041,0.000917889479732164,-0.00162935337711587));
#29108=CARTESIAN_POINT('',(-0.00458473802636611,0.00161880142913698,-0.00159307813775496));
#29109=CARTESIAN_POINT('',(-0.00392243184051651,0.00287170398310953,-0.00152056639685241));
#29110=CARTESIAN_POINT('',(-0.00345264644635402,0.00342311019951849,-0.00148446707997406));
#29111=CARTESIAN_POINT('',(-0.00231729913548722,0.00427363416208182,-0.00141179550015312));
#29112=CARTESIAN_POINT('',(-0.00165738540690224,0.00457042975695331,-0.00137578503462994));
#29113=CARTESIAN_POINT('',(-0.000267020440625006,0.00485440350324129,-0.00130305997002273));
#29114=CARTESIAN_POINT('',(0.000456427476013587,0.00483994949352714,-0.00126704928265082));
#29115=CARTESIAN_POINT('',(0.00183435335107614,0.00450271828511218,-0.00119437823904703));
#29116=CARTESIAN_POINT('',(0.00248268968913113,0.00417954622329636,-0.00115827834973921));
#29117=CARTESIAN_POINT('',(0.00358317565607457,0.00328660442612778,-0.00108576745752035));
#29118=CARTESIAN_POINT('',(0.00403196568092297,0.0027159274634508,-0.00104949156799179));
#29119=CARTESIAN_POINT('',(0.00464388105096199,0.00144017841039315,-0.000977243094286331));
#29120=CARTESIAN_POINT('',(0.00480647376858471,0.000730306838074866,-0.000940708962314518));
#29121=CARTESIAN_POINT('',(0.00481346911222684,-0.000681562507469895,-0.00086881823594223));
#29122=CARTESIAN_POINT('',(0.00465825553960098,-0.00139305428604988,-0.000832284398307179));
#29123=CARTESIAN_POINT('',(0.00405919834765599,-0.00267489142155171,-0.000760035195297809));
#29124=CARTESIAN_POINT('',(0.00361625713726488,-0.00325008079200467,-0.000723759955934081));
#29125=CARTESIAN_POINT('',(0.00252490095813153,-0.00415415821337312,-0.000651248215036885));
#29126=CARTESIAN_POINT('',(0.00187986182427066,-0.00448381204369751,-0.000615148898156361));
#29127=CARTESIAN_POINT('',(0.000505456252165614,-0.00483511511877466,-0.000542477318334643));
#29128=CARTESIAN_POINT('',(-0.000217803291853572,-0.0048567804434947,-0.000506466852810241));
#29129=CARTESIAN_POINT('',(-0.00161100507485052,-0.00458706833792599,-0.000433741788206097));
#29130=CARTESIAN_POINT('',(-0.00227385248782081,-0.00429686304231336,-0.000397731100828119));
#29131=CARTESIAN_POINT('',(-0.0034178372047709,-0.00345799262771901,-0.000325060057233522));
#29132=CARTESIAN_POINT('',(-0.00389314928382333,-0.00291131299915446,-0.000288960167921819));
#29133=CARTESIAN_POINT('',(-0.00456815171265774,-0.00166520460192758,-0.000216449275701425));
#29134=CARTESIAN_POINT('',(-0.00476439101216319,-0.000966223329313042,-0.000180173386168644));
#29135=CARTESIAN_POINT('',(-0.00484151907170559,0.000446584983549208,-0.000107924912473147));
#29136=CARTESIAN_POINT('',(-0.00472007906582131,0.00116464233918359,-7.13907804971041E-5));
#29137=CARTESIAN_POINT('',(-0.00418624291343246,0.00247171653222957,4.99945876723195E-7));
#29138=CARTESIAN_POINT('',(-0.00377056815458997,0.003069651561286,3.70337835121602E-5));
#29139=CARTESIAN_POINT('',(-0.00272657364139774,0.00402466539239435,0.00010928298651923));
#29140=CARTESIAN_POINT('',(-0.00209723388046976,0.00438656481634434,0.000145558225883721));
#29141=CARTESIAN_POINT('',(-0.000742976793153477,0.00480417951318895,0.000218069966781685));
#29142=CARTESIAN_POINT('',(-2.0885280432126E-5,0.00486189415008451,0.000254169283662596));
#29143=CARTESIAN_POINT('',(0.00138333776357875,0.00466049362906015,0.000326840863482779));
#29144=CARTESIAN_POINT('',(0.00205983341381665,0.0044037303343389,0.000362851329005269));
#29145=CARTESIAN_POINT('',(0.00324376967147804,0.00362139360003873,0.000435576393614782));
#29146=CARTESIAN_POINT('',(0.00374510407088124,0.00309961814406744,0.00047158708098969));
#29147=CARTESIAN_POINT('',(0.00448098632681381,0.00188681893953618,0.000544258124585055));
#29148=CARTESIAN_POINT('',(0.0047109121915401,0.00119985876201141,0.000580358013895203));
#29149=CARTESIAN_POINT('',(0.00485766808138741,-0.000209707527801439,0.000652868906117898));
#29150=CARTESIAN_POINT('',(0.00477148100111083,-0.000930579547875692,0.000689144795648389));
#29151=CARTESIAN_POINT('',(0.00430207970226465,-0.00226535986205061,0.000761393269346187));
#29152=CARTESIAN_POINT('',(0.00391509511291008,-0.00288228527780993,0.000797927401320691));
#29153=CARTESIAN_POINT('',(0.00292169917945418,-0.00388557412112409,0.000869818127695285));
#29154=CARTESIAN_POINT('',(0.00230884594832506,-0.00427892221277948,0.000906351965326132));
#29155=CARTESIAN_POINT('',(0.000978852814690916,-0.00476172054092505,0.000978601168341638));
#29156=CARTESIAN_POINT('',(0.000258925776844741,-0.00485523411170611,0.00101487640770113));
#29157=CARTESIAN_POINT('',(-0.00115205885348002,-0.00472280803211599,0.00108738814860063));
#29158=CARTESIAN_POINT('',(-0.00184127085802862,-0.00449979694529959,0.00112348746547846));
#29159=CARTESIAN_POINT('',(-0.00306153114480408,-0.00377635423180277,0.00119615904530325));
#29160=CARTESIAN_POINT('',(-0.0035882725709651,-0.00328025220169392,0.00123216951082539));
#29161=CARTESIAN_POINT('',(-0.00438269974046544,-0.00210439451456205,0.00130489457543106));
#29162=CARTESIAN_POINT('',(-0.00464619750860506,-0.00143048448149263,0.00134090526280791));
#29163=CARTESIAN_POINT('',(-0.00486194590083901,-2.83941718649549E-5,0.00141357630640327));
#29164=CARTESIAN_POINT('',(-0.0048114814226229,0.000694263094889662,0.00144967619571505));
#29165=CARTESIAN_POINT('',(-0.00440764851959346,0.00205269358742906,0.00152218708793468));
#29166=CARTESIAN_POINT('',(-0.00405215626119944,0.0026857101246911,0.00155846297747023));
#29167=CARTESIAN_POINT('',(-0.00310768769666081,0.00373925423700836,0.00163071145114705));
#29168=CARTESIAN_POINT('',(-0.00251407341960766,0.00416112641070731,0.00166724558321998));
#29169=CARTESIAN_POINT('',(-0.0012123532301178,0.00470788827330421,0.00173913630957742));
#29170=CARTESIAN_POINT('',(-0.000495622876939057,0.00483676574602459,0.00177567014631293));
#29171=CARTESIAN_POINT('',(0.000917889477907517,0.0047738469014571,0.00184791935053893));
#29172=CARTESIAN_POINT('',(0.00161880143500428,0.00458473802439018,0.00188419459299961));
#29173=CARTESIAN_POINT('',(0.00287170398482693,0.00392243184277044,0.00195670632674376));
#29174=CARTESIAN_POINT('',(0.00342311018306367,0.0034526464567348,0.00199280563664444));
#29175=CARTESIAN_POINT('',(0.00427363417322163,0.00231729911780535,0.00206547725050609));
#29176=CARTESIAN_POINT('',(0.00457042977174294,0.00165738541607217,0.00210148771169285));
#29177=CARTESIAN_POINT('',(0.00485440343966745,0.000267020530351741,0.00217421263830122));
#29178=CARTESIAN_POINT('',(0.00483994947871846,-0.000456427850068477,0.00221022347312812));
#29179=CARTESIAN_POINT('',(0.00450271857873417,-0.00183435351687859,0.00228289499949617));
#29180=CARTESIAN_POINT('',(0.00417954681684493,-0.00248268734221482,0.00231899393251005));
#29181=CARTESIAN_POINT('',(0.00328660218651989,-0.0035831764053507,0.0023915033797381));
#29182=CARTESIAN_POINT('',(0.00271592340140939,-0.00403197462474551,0.0024277835632829));
#29183=CARTESIAN_POINT('',(0.00144019517612842,-0.00464387514350149,0.0025000356117708));
#29184=CARTESIAN_POINT('',(0.000730316340889192,-0.00480643860397344,0.00253653941438567));
#29185=CARTESIAN_POINT('',(-0.00123075016520761,-0.00481623257959065,0.00263642085553527));
#29186=CARTESIAN_POINT('',(-0.00249186065161184,-0.00430099307276901,0.00270163700098398));
#29187=CARTESIAN_POINT('',(-0.00427649949251748,-0.00253521549583444,0.00282965584356534));
#29188=CARTESIAN_POINT('',(-0.00480374912175907,-0.00126752528841583,0.00289545230430405));
#29189=CARTESIAN_POINT('',(-0.00480994288355359,-2.43665513178439E-5,0.00295881582269299));
#29190=CARTESIAN_POINT('',(-0.00481,2.43712308653186E-5,-0.0152300713606537));
#29191=CARTESIAN_POINT('',(-0.00480690252434544,0.000645958221424933,-0.015198389586565));
#29192=CARTESIAN_POINT('',(-0.00467712430393056,0.00128470170063566,-0.0151654813513713));
#29193=CARTESIAN_POINT('',(-0.00388793251657289,0.00316730242218104,-0.0150617853642725));
#29194=CARTESIAN_POINT('',(-0.00273168049484676,0.00420588673001337,-0.014988829115302));
#29195=CARTESIAN_POINT('',(-0.000694345269151162,0.00481158888805761,-0.0148800363035863));
#29196=CARTESIAN_POINT('',(2.83713107815876E-5,0.00486198731371525,-0.0148439092190894));
#29197=CARTESIAN_POINT('',(0.0014305306932682,0.00464623359414285,-0.0147712492556481));
#29198=CARTESIAN_POINT('',(0.00210442685798093,0.00438275491925437,-0.0147352455159436));
#29199=CARTESIAN_POINT('',(0.00328028975549539,0.00358831715552897,-0.014662515643209));
#29200=CARTESIAN_POINT('',(0.00377640149651015,0.00306156230762301,-0.0146265042621575));
#29201=CARTESIAN_POINT('',(0.00449985258902826,0.00184128806164442,-0.0145538343796196));
#29202=CARTESIAN_POINT('',(0.00472286532095683,0.00115206864444611,-0.0145177348671644));
#29203=CARTESIAN_POINT('',(0.00485529143886879,-0.000258933307440913,-0.0144452226301512));
#29204=CARTESIAN_POINT('',(0.00476177621900751,-0.000978868749884339,-0.0144089475733588));
#29205=CARTESIAN_POINT('',(0.004278970983756,-0.00230887726412092,-0.0143366984883185));
#29206=CARTESIAN_POINT('',(0.00388561768822807,-0.00292173733364788,-0.0143001645803893));
#29207=CARTESIAN_POINT('',(0.00288231585551244,-0.00391514436671711,-0.0142282738188832));
#29208=CARTESIAN_POINT('',(0.00226538287099962,-0.00430213287315544,-0.014191739718195));
#29209=CARTESIAN_POINT('',(0.00093058617559742,-0.00477153857116873,-0.0141194912327727));
#29210=CARTESIAN_POINT('',(0.000209705532278956,-0.00485772598627435,-0.0140832153449124));
#29211=CARTESIAN_POINT('',(-0.00119987733461742,-0.0047109670668637,-0.0140107044565176));
#29212=CARTESIAN_POINT('',(-0.00188684551851613,-0.00448103781073583,-0.0139746045613348));
#29213=CARTESIAN_POINT('',(-0.00309965835778344,-0.00374514575282502,-0.0139019335286979));
#29214=CARTESIAN_POINT('',(-0.00362143963251185,-0.00324380485226769,-0.0138659228311588));
#29215=CARTESIAN_POINT('',(-0.00440378449138592,-0.00205985392237314,-0.0137931977801048));
#29216=CARTESIAN_POINT('',(-0.00466055027259019,-0.0013833499116694,-0.0137571873044536));
#29217=CARTESIAN_POINT('',(-0.0048619518764676,2.0889889465098E-5,-0.0136845157355505));
#29218=CARTESIAN_POINT('',(-0.00480423591641779,0.000742989987634153,-0.0136484164128556));
#29219=CARTESIAN_POINT('',(-0.00438661502827952,0.00209726275005554,-0.0135759046751557));
#29220=CARTESIAN_POINT('',(-0.00402471076561506,0.00272660964436907,-0.0135396294384451));
#29221=CARTESIAN_POINT('',(-0.00306968457802422,0.00377061576744125,-0.0134673802260291));
#29222=CARTESIAN_POINT('',(-0.00247174219745113,0.00418629483787636,-0.0134308464034582));
#29223=CARTESIAN_POINT('',(-0.00116465174556414,0.00472013627090797,-0.0133589556504941));
#29224=CARTESIAN_POINT('',(-0.000446585888062056,0.00484157699819559,-0.0133224215335274));
#29225=CARTESIAN_POINT('',(0.000966239236385627,0.00476444673805005,-0.0132501730505603));
#29226=CARTESIAN_POINT('',(0.00166522860381854,0.00456820444675366,-0.0132138971635795));
#29227=CARTESIAN_POINT('',(0.00291135115826841,0.00389319287385263,-0.0131413862746769));
#29228=CARTESIAN_POINT('',(0.00345803688564065,0.00341787459831736,-0.0131052863794496));
#29229=CARTESIAN_POINT('',(0.00429691614588139,0.0022738756080041,-0.0130326153469013));
#29230=CARTESIAN_POINT('',(0.00458712432947191,0.00161101996177957,-0.0129966046493296));
#29231=CARTESIAN_POINT('',(0.00485683832637343,0.000217801514243265,-0.0129238795982987));
#29232=CARTESIAN_POINT('',(0.00483517209944476,-0.000505466705321743,-0.0128878691226277));
#29233=CARTESIAN_POINT('',(0.00448386361212515,-0.00187988817339661,-0.0128151975537403));
#29234=CARTESIAN_POINT('',(0.00415420527386462,-0.00252493473283444,-0.0127790982310671));
#29235=CARTESIAN_POINT('',(0.00325011613385979,-0.00361630302454977,-0.0127065864933079));
#29236=CARTESIAN_POINT('',(0.00267491956319904,-0.00405924897364133,-0.0126703112566191));
#29237=CARTESIAN_POINT('',(0.00139306656888672,-0.00465831216310324,-0.0125980620442184));
#29238=CARTESIAN_POINT('',(0.000681566348417449,-0.00481352690581254,-0.0125615282216268));
#29239=CARTESIAN_POINT('',(-0.000730320039149999,-0.00480653021885982,-0.0124896374686892));
#29240=CARTESIAN_POINT('',(-0.00144019974224342,-0.00464393491420252,-0.0124531033517134));
#29241=CARTESIAN_POINT('',(-0.00271596348504431,-0.00403201107755429,-0.0123808548687378));
#29242=CARTESIAN_POINT('',(-0.00328664678144064,-0.00358321519089635,-0.0123445789817365));
#29243=CARTESIAN_POINT('',(-0.00417959815891117,-0.00248271535820966,-0.0122720680928834));
#29244=CARTESIAN_POINT('',(-0.00450277348399899,-0.00183437096143296,-0.0122359681976468));
#29245=CARTESIAN_POINT('',(-0.00484000740253075,-0.000456428514420108,-0.0121632971650678));
#29246=CARTESIAN_POINT('',(-0.00485446092968617,0.000267028113936751,-0.0121272864675541));
#29247=CARTESIAN_POINT('',(-0.0045704825534782,0.00165740920001288,-0.012054561416438));
#29248=CARTESIAN_POINT('',(-0.00427368280511274,0.00231733059850723,-0.0120185509408203));
#29249=CARTESIAN_POINT('',(-0.00342314775915248,0.00345269052415205,-0.0119458793719114));
#29250=CARTESIAN_POINT('',(-0.00287173453630625,0.00392248105352976,-0.0119097800492129));
#29251=CARTESIAN_POINT('',(-0.00161881652045838,0.004584793945446,-0.0118372683115257));
#29252=CARTESIAN_POINT('',(-0.000917896105497493,0.00477390444385893,-0.0118009930747972));
#29253=CARTESIAN_POINT('',(0.000495633197181967,0.00483682275963525,-0.0117287438624042));
#29254=CARTESIAN_POINT('',(0.00121237179874327,0.00470794313706156,-0.0116922100397982));
#29255=CARTESIAN_POINT('',(0.00251410721827715,0.00416117351230247,-0.0116203192868814));
#29256=CARTESIAN_POINT('',(0.00310772801722916,0.00373929583689428,-0.0115837851698876));
#29257=CARTESIAN_POINT('',(0.00405220691337471,0.00268573828077846,-0.0115115366869274));
#29258=CARTESIAN_POINT('',(0.00440770278012855,0.00205271390416126,-0.0114752607999356));
#29259=CARTESIAN_POINT('',(0.00481153922799867,0.000694266935140251,-0.011402749911048));
#29260=CARTESIAN_POINT('',(0.00486200363716491,-2.83990257214252E-5,-0.0113666500158559));
#29261=CARTESIAN_POINT('',(0.00464625140691769,-0.00143050568293938,-0.0112939789832225));
#29262=CARTESIAN_POINT('',(0.00438274985912934,-0.00210442357992527,-0.0112579682857279));
#29263=CARTESIAN_POINT('',(0.00358831224336821,-0.0032802943880181,-0.0111852432346279));
#29264=CARTESIAN_POINT('',(0.00306156404473304,-0.0037764019147314,-0.0111492327590233));
#29265=CARTESIAN_POINT('',(0.00184128869076233,-0.00449985204131579,-0.0110765611900722));
#29266=CARTESIAN_POINT('',(0.00115206824794929,-0.00472286519122483,-0.0110404618674185));
#29267=CARTESIAN_POINT('',(-0.000258933233588031,-0.00485529154938711,-0.0109679501296838));
#29268=CARTESIAN_POINT('',(-0.000978868713517307,-0.00476177623805386,-0.0109316748929821));
#29269=CARTESIAN_POINT('',(-0.00230887730190845,-0.00427897093691872,-0.010859425680583));
#29270=CARTESIAN_POINT('',(-0.00292173732970695,-0.00388561770330084,-0.0108228918579371));
#29271=CARTESIAN_POINT('',(-0.00391514436387597,-0.00288231585963184,-0.0107510011051061));
#29272=CARTESIAN_POINT('',(-0.00430213287321797,-0.00226538286521935,-0.0107144669880661));
#29273=CARTESIAN_POINT('',(-0.00477153857249349,-0.000930586177030942,-0.0106422185051128));
#29274=CARTESIAN_POINT('',(-0.00485772598645182,-0.000209705533414721,-0.0106059426180949));
#29275=CARTESIAN_POINT('',(-0.00471096706635025,0.00119987733525803,-0.0105334317292525));
#29276=CARTESIAN_POINT('',(-0.00448103781074004,0.00188684551865477,-0.010497331834055));
#29277=CARTESIAN_POINT('',(-0.00374514575298108,0.00309965835763356,-0.0104246608013869));
#29278=CARTESIAN_POINT('',(-0.00324380485225424,0.00362143963252127,-0.0103886501039201));
#29279=CARTESIAN_POINT('',(-0.002059853922329,0.00440378449138652,-0.0103159250527994));
#29280=CARTESIAN_POINT('',(-0.00138334991168053,0.00466055027259388,-0.0102799145771913));
#29281=CARTESIAN_POINT('',(2.08898894649507E-5,0.00486195187646364,-0.0102072430082677));
#29282=CARTESIAN_POINT('',(0.000742989987636098,0.00480423591641733,-0.0101711436855808));
#29283=CARTESIAN_POINT('',(0.00209726275005457,0.00438661502828031,-0.0100986319478852));
#29284=CARTESIAN_POINT('',(0.00272660964436737,0.0040247107656129,-0.0100623567111655));
#29285=CARTESIAN_POINT('',(0.00377061576744357,0.00306968457802569,-0.00999010749876331));
#29286=CARTESIAN_POINT('',(0.00418629483786854,0.00247174219744889,-0.00995357367616607));
#29287=CARTESIAN_POINT('',(0.00472013627091582,0.00116465174556636,-0.00988168292324078));
#29288=CARTESIAN_POINT('',(0.00484157699820177,0.000446585888060814,-0.00984514880626354));
#29289=CARTESIAN_POINT('',(0.00476444673804396,-0.000966239236384054,-0.00977290032327878));
#29290=CARTESIAN_POINT('',(0.00456820444675509,-0.00166522860381626,-0.00973662443630273));
#29291=CARTESIAN_POINT('',(0.00389319287385112,-0.00291135115827085,-0.00966411354740819));
#29292=CARTESIAN_POINT('',(0.00341787459832332,-0.00345803688565274,-0.00962801365220536));
#29293=CARTESIAN_POINT('',(0.00227387560799953,-0.00429691614586831,-0.00955534261960021));
#29294=CARTESIAN_POINT('',(0.00161101996178304,-0.00458712432948514,-0.00951933192208457));
#29295=CARTESIAN_POINT('',(0.000217801514241914,-0.0048568383263598,-0.00944660687099837));
#29296=CARTESIAN_POINT('',(-0.000505466705321383,-0.00483517209944751,-0.00941059639536392));
#29297=CARTESIAN_POINT('',(-0.00187988817339405,-0.00448386361212312,-0.00933792482645878));
#29298=CARTESIAN_POINT('',(-0.00252493473283018,-0.00415420527386074,-0.00930182550378328));
#29299=CARTESIAN_POINT('',(-0.00361630302455418,-0.00325011613386351,-0.00922931376604625));
#29300=CARTESIAN_POINT('',(-0.00405924897363877,-0.002674919563202,-0.00919303852934839));
#29301=CARTESIAN_POINT('',(-0.00465831216310405,-0.00139306656888755,-0.00912078931694394));
#29302=CARTESIAN_POINT('',(-0.00481352690581081,-0.000681566348417764,-0.00908425549434557));
#29303=CARTESIAN_POINT('',(-0.00480653021886154,0.000730320039150845,-0.00901236474142489));
#29304=CARTESIAN_POINT('',(-0.00464393491419733,0.00144019974223911,-0.00897583062442999));
#29305=CARTESIAN_POINT('',(-0.00403201107756128,0.0027159634850448,-0.00890358214147594));
#29306=CARTESIAN_POINT('',(-0.00358321519089434,0.00328664678143411,-0.00886730625445426));
#29307=CARTESIAN_POINT('',(-0.00248271535821132,0.00417959815891801,-0.0087947953656203));
#29308=CARTESIAN_POINT('',(-0.0018343709614343,0.00450277348399542,-0.00875869547037181));
#29309=CARTESIAN_POINT('',(-0.000456428514422146,0.00484000740253341,-0.00868602443779733));
#29310=CARTESIAN_POINT('',(0.000267028113934224,0.00485446092967978,-0.00865001374026796));
#29311=CARTESIAN_POINT('',(0.00165740920001532,0.00457048255348461,-0.00857728868917869));
#29312=CARTESIAN_POINT('',(0.00231733059850565,0.00427368280511121,-0.008541278213545));
#29313=CARTESIAN_POINT('',(0.00345269052415222,0.00342314775915501,-0.0084686066446414));
#29314=CARTESIAN_POINT('',(0.00392248105353805,0.00287173453631088,-0.00843250732196013));
#29315=CARTESIAN_POINT('',(0.00458479394543713,0.00161881652045476,-0.00835999558423306));
#29316=CARTESIAN_POINT('',(0.00477390444385966,0.000917896105497934,-0.00832372034752825));
#29317=CARTESIAN_POINT('',(0.00483682275963445,-0.000495633197182035,-0.00825147113512762));
#29318=CARTESIAN_POINT('',(0.00470794313705902,-0.00121237179874085,-0.00821493731251739));
#29319=CARTESIAN_POINT('',(0.00416117351230491,-0.00251410721827962,-0.00814304655961665));
#29320=CARTESIAN_POINT('',(0.00373929583689171,-0.00310772801722806,-0.00810651244261374));
#29321=CARTESIAN_POINT('',(0.00268573828078122,-0.00405220691337558,-0.00803426395965584));
#29322=CARTESIAN_POINT('',(0.0020527139041605,-0.00440770278012326,-0.00799798807265104));
#29323=CARTESIAN_POINT('',(0.000694266935141895,-0.00481153922800366,-0.00792547718378718));
#29324=CARTESIAN_POINT('',(-2.83990257172541E-5,-0.00486200363715717,-0.00788937728856627));
#29325=CARTESIAN_POINT('',(-0.00143050568294196,-0.00464625140692552,-0.00781670625596649));
#29326=CARTESIAN_POINT('',(-0.00210442357991806,-0.0043827498591222,-0.00778069555843515));
#29327=CARTESIAN_POINT('',(-0.0032802943880256,-0.00358831224337504,-0.00770797050737502));
#29328=CARTESIAN_POINT('',(-0.00377640191471928,-0.00306156404472798,-0.00767196003172528));
#29329=CARTESIAN_POINT('',(-0.00449985204132647,-0.00184128869076967,-0.00759928846282476));
#29330=CARTESIAN_POINT('',(-0.00472286519121385,-0.00115206824794936,-0.00756318914012465));
#29331=CARTESIAN_POINT('',(-0.00485529154939798,0.000258933233587683,-0.00749067740243213));
#29332=CARTESIAN_POINT('',(-0.00476177623805565,0.000978868713516223,-0.0074544021657163));
#29333=CARTESIAN_POINT('',(-0.00427897093691827,0.00230887730190563,-0.00738215295330343));
#29334=CARTESIAN_POINT('',(-0.00388561770330705,0.00292173732971719,-0.00734561913069079));
#29335=CARTESIAN_POINT('',(-0.00288231585962521,0.00391514436386607,-0.00727372837780692));
#29336=CARTESIAN_POINT('',(-0.0022653828652209,0.00430213287321315,-0.00723719426078343));
#29337=CARTESIAN_POINT('',(-0.000930586177033348,0.0047715385724968,-0.00716494577785006));
#29338=CARTESIAN_POINT('',(-0.000209705533413502,0.00485772598645561,-0.00712866989082981));
#29339=CARTESIAN_POINT('',(0.00119987733525716,0.00471096706634635,-0.00705615900197206));
#29340=CARTESIAN_POINT('',(0.00188684551863979,0.00448103781072474,-0.00702005910673978));
#29341=CARTESIAN_POINT('',(0.003099658357646,0.00374514575299788,-0.00694738807415686));
#29342=CARTESIAN_POINT('',(0.00362143963251041,0.00324380485225148,-0.00691137737662819));
#29343=CARTESIAN_POINT('',(0.0044037844913961,0.00205985392233354,-0.00683865232554582));
#29344=CARTESIAN_POINT('',(0.00466055027259315,0.00138334991168341,-0.00680264184991632));
#29345=CARTESIAN_POINT('',(0.00486195187646409,-2.0889889466212E-5,-0.00672997028099736));
#29346=CARTESIAN_POINT('',(0.00480423591642111,-0.000742989987636956,-0.00669387095831539));
#29347=CARTESIAN_POINT('',(0.0043866150282763,-0.00209726275005415,-0.00662135922060507));
#29348=CARTESIAN_POINT('',(0.0040247107656172,-0.00272660964437124,-0.00658508398390573));
#29349=CARTESIAN_POINT('',(0.00306968457802141,-0.00377061576743955,-0.0065128347714775));
#29350=CARTESIAN_POINT('',(0.00247174219744538,-0.0041862948378624,-0.0064763009488776));
#29351=CARTESIAN_POINT('',(0.00116465174556965,-0.00472013627092198,-0.00640441019598375));
#29352=CARTESIAN_POINT('',(0.000446585888064109,-0.00484157699819391,-0.0063678760789755));
#29353=CARTESIAN_POINT('',(-0.000966239236386695,-0.00476444673805183,-0.00629562759602143));
#29354=CARTESIAN_POINT('',(-0.00166522860381339,-0.0045682044467502,-0.00625935170901975));
#29355=CARTESIAN_POINT('',(-0.00291135115827368,-0.00389319287385601,-0.00618684082014577));
#29356=CARTESIAN_POINT('',(-0.00345803688564666,-0.00341787459832007,-0.00615074092491954));
#29357=CARTESIAN_POINT('',(-0.00429691614587471,-0.00227387560800222,-0.00607806989234047));
#29358=CARTESIAN_POINT('',(-0.00458712432948343,-0.00161101996178013,-0.00604205919480918));
#29359=CARTESIAN_POINT('',(-0.00485683832636154,-0.000217801514244552,-0.00596933414372833));
#29360=CARTESIAN_POINT('',(-0.00483517209945259,0.000505466705323897,-0.00593332366809922));
#29361=CARTESIAN_POINT('',(-0.00448386361211786,0.00187988817339216,-0.00586065209917797));
#29362=CARTESIAN_POINT('',(-0.00415420527385522,0.00252493473282551,-0.00582455277649567));
#29363=CARTESIAN_POINT('',(-0.00325011613386882,0.00361630302455911,-0.00575204103878842));
#29364=CARTESIAN_POINT('',(-0.0026749195632004,0.00405924897363534,-0.00571576580206647));
#29365=CARTESIAN_POINT('',(-0.00139306656888904,0.00465831216310752,-0.00564351658968042));
#29366=CARTESIAN_POINT('',(-0.000681566348418915,0.00481352690578914,-0.0056069827670533));
#29367=CARTESIAN_POINT('',(0.000730320039152311,0.00480653021888319,-0.00553509201417171));
#29368=CARTESIAN_POINT('',(0.00144019974223843,0.00464393491419858,-0.0054985578971569));
#29369=CARTESIAN_POINT('',(0.00271596348504603,0.00403201107755983,-0.00542630941420362));
#29370=CARTESIAN_POINT('',(0.00328664678144265,0.00358321519089882,-0.00539003352719887));
#29371=CARTESIAN_POINT('',(0.00417959815890971,0.00248271535820656,-0.00531752263833027));
#29372=CARTESIAN_POINT('',(0.00450277348400127,0.00183437096143369,-0.00528142274310945));
#29373=CARTESIAN_POINT('',(0.00484000740252775,0.000456428514422211,-0.00520875171051427));
#29374=CARTESIAN_POINT('',(0.00485446092967311,-0.000267028113933861,-0.00517274101298296));
#29375=CARTESIAN_POINT('',(0.00457048255349136,-0.00165740920001511,-0.00510001596191823));
#29376=CARTESIAN_POINT('',(0.00427368280511466,-0.00231733059850962,-0.00506400548628336));
#29377=CARTESIAN_POINT('',(0.00342314775915118,-0.00345269052414871,-0.00499133391735751));
#29378=CARTESIAN_POINT('',(0.00287173453630816,-0.00392248105353095,-0.00495523459467405));
#29379=CARTESIAN_POINT('',(0.00161881652045694,-0.00458479394544451,-0.0048827228569737));
#29380=CARTESIAN_POINT('',(0.000917896105497196,-0.00477390444386005,-0.00484644762025596));
#29381=CARTESIAN_POINT('',(-0.00049563319718127,-0.00483682275963408,-0.00477419840785456));
#29382=CARTESIAN_POINT('',(-0.00121237179874249,-0.00470794313706126,-0.00473766458524968));
#29383=CARTESIAN_POINT('',(-0.00251410721827838,-0.00416117351230251,-0.00466577383233895));
#29384=CARTESIAN_POINT('',(-0.00310772801722835,-0.00373929583689227,-0.00462923971534218));
#29385=CARTESIAN_POINT('',(-0.00405220691337581,-0.0026857382807801,-0.00455699123238198));
#29386=CARTESIAN_POINT('',(-0.00440770278012495,-0.00205271390416107,-0.00452071534538068));
#29387=CARTESIAN_POINT('',(-0.00481153922800245,-0.000694266935139741,-0.00444820445651207));
#29388=CARTESIAN_POINT('',(-0.00486200363715706,2.83990257185022E-5,-0.00441210456129357));
#29389=CARTESIAN_POINT('',(-0.00464625140692539,0.00143050568294268,-0.00433943352869379));
#29390=CARTESIAN_POINT('',(-0.0043827498591258,0.00210442357992084,-0.00430342283117053));
#29391=CARTESIAN_POINT('',(-0.00358831224337125,0.00328029438802319,-0.00423069778009429));
#29392=CARTESIAN_POINT('',(-0.00306156404472769,0.00377640191472449,-0.00419468730445865));
#29393=CARTESIAN_POINT('',(-0.0018412886907671,0.00449985204132296,-0.00412201573554585));
#29394=CARTESIAN_POINT('',(-0.00115206824794905,0.00472286519122003,-0.00408591641286201));
#29395=CARTESIAN_POINT('',(0.000258933233587908,0.00485529154939188,-0.00401340467514939));
#29396=CARTESIAN_POINT('',(0.000978868713518797,0.00476177623805698,-0.00397712943844506));
#29397=CARTESIAN_POINT('',(0.00230887730190647,0.0042789709369157,-0.0039048802260291));
#29398=CARTESIAN_POINT('',(0.00292173732971809,0.00388561770330835,-0.00386834640341961));
#29399=CARTESIAN_POINT('',(0.00391514436386531,0.00288231585962375,-0.00379645565053266));
#29400=CARTESIAN_POINT('',(0.0043021328732162,0.0022653828652185,-0.00375992153351668));
#29401=CARTESIAN_POINT('',(0.00477153857249563,0.000930586177030387,-0.00368767305057105));
#29402=CARTESIAN_POINT('',(0.00485772598645863,0.000209705533410371,-0.0036513971635648));
#29403=CARTESIAN_POINT('',(0.00471096706634329,-0.0011998773352544,-0.00357888627469158));
#29404=CARTESIAN_POINT('',(0.00448103781072517,-0.00188684551864377,-0.00354278637947381));
#29405=CARTESIAN_POINT('',(0.00374514575299448,-0.0030996583576469,-0.00347011534687709));
#29406=CARTESIAN_POINT('',(0.00324380485224853,-0.00362143963250802,-0.00343410464934653));
#29407=CARTESIAN_POINT('',(0.00205985392233213,-0.00440378449140138,-0.00336137959828178));
#29408=CARTESIAN_POINT('',(0.00138334991167975,-0.00466055027259318,-0.00332536912264461));
#29409=CARTESIAN_POINT('',(-2.08898894681853E-5,-0.00486195187646488,-0.00325269755372335));
#29410=CARTESIAN_POINT('',(-0.00074298998763811,-0.00480423591642181,-0.00321659823104266));
#29411=CARTESIAN_POINT('',(-0.00209726275005327,-0.0043866150282755,-0.00314408649333233));
#29412=CARTESIAN_POINT('',(-0.00272660964437155,-0.00402471076561353,-0.00310781125662636));
#29413=CARTESIAN_POINT('',(-0.0037706157674433,-0.00306968457802139,-0.00303556204421116));
#29414=CARTESIAN_POINT('',(-0.00418629483786456,-0.00247174219744504,-0.00299902822160718));
#29415=CARTESIAN_POINT('',(-0.0047201362709199,-0.00116465174556981,-0.00292713746870873));
#29416=CARTESIAN_POINT('',(-0.00484157699819433,-0.000446585888059789,-0.00289060335170224));
#29417=CARTESIAN_POINT('',(-0.00476444673805111,0.000966239236387943,-0.00281835486874896));
#29418=CARTESIAN_POINT('',(-0.00456820444675054,0.00166522860381336,-0.00278207898174626));
#29419=CARTESIAN_POINT('',(-0.0038931928738557,0.00291135115827364,-0.00270956809287382));
#29420=CARTESIAN_POINT('',(-0.00341787459832011,0.00345803688565272,-0.00267346819765328));
#29421=CARTESIAN_POINT('',(-0.00227387560799978,0.00429691614587045,-0.00260079716506118));
#29422=CARTESIAN_POINT('',(-0.00161101996178054,0.00458712432948444,-0.00256478646753567));
#29423=CARTESIAN_POINT('',(-0.00021780151424385,0.00485683832636059,-0.00249206141645638));
#29424=CARTESIAN_POINT('',(0.000505466705324944,0.00483517209945441,-0.00245605094083143));
#29425=CARTESIAN_POINT('',(0.00187988817339327,0.0044838636121155,-0.00238337937190023));
#29426=CARTESIAN_POINT('',(0.00252493473282808,0.00415420527385413,-0.00234728004922253));
#29427=CARTESIAN_POINT('',(0.00361630302455786,0.00325011613386882,-0.00227476831151606));
#29428=CARTESIAN_POINT('',(0.00405924897364287,0.00267491956320294,-0.00223849307480867));
#29429=CARTESIAN_POINT('',(0.00465831216310039,0.00139306656888563,-0.00216624386239272));
#29430=CARTESIAN_POINT('',(0.00481352690579794,0.000681566348418114,-0.00212971003978478));
#29431=CARTESIAN_POINT('',(0.00480653021887437,-0.000730320039151922,-0.00205781928689476));
#29432=CARTESIAN_POINT('',(0.00464393491419765,-0.00144019974223965,-0.00202128516988457));
#29433=CARTESIAN_POINT('',(0.00403201107756084,-0.00271596348504455,-0.00194903668693051));
#29434=CARTESIAN_POINT('',(0.00358321519089824,-0.00328664678144329,-0.00191276079992653));
#29435=CARTESIAN_POINT('',(0.00248271535820694,-0.00417959815890921,-0.00184024991105715));
#29436=CARTESIAN_POINT('',(0.00183437096143363,-0.00450277348400167,-0.00180415001583673));
#29437=CARTESIAN_POINT('',(0.000456428514421963,-0.00484000740252739,-0.00173147898324156));
#29438=CARTESIAN_POINT('',(-0.000267028113935476,-0.00485446092967608,-0.00169546828571443));
#29439=CARTESIAN_POINT('',(-0.00165740920001464,-0.00457048255348819,-0.00162274323464126));
#29440=CARTESIAN_POINT('',(-0.00231733059850924,-0.00427368280511491,-0.00158673275900833));
#29441=CARTESIAN_POINT('',(-0.0034526905241487,-0.00342314775915125,-0.00151406119008708));
#29442=CARTESIAN_POINT('',(-0.0039224810535339,-0.0028717345363086,-0.00147796186740589));
#29443=CARTESIAN_POINT('',(-0.00458479394544172,-0.00161881652045623,-0.00140545012969634));
#29444=CARTESIAN_POINT('',(-0.00477390444386256,-0.000917896105497446,-0.00136917489298627));
#29445=CARTESIAN_POINT('',(-0.0048368227596316,0.000495633197181834,-0.00129692568057875));
#29446=CARTESIAN_POINT('',(-0.00470794313705758,0.00121237179874062,-0.00126039185796734));
#29447=CARTESIAN_POINT('',(-0.00416117351230611,0.00251410721828054,-0.00118850110507579));
#29448=CARTESIAN_POINT('',(-0.00373929583689225,0.00310772801722703,-0.00115196698806636));
#29449=CARTESIAN_POINT('',(-0.0026857382807799,0.00405220691337737,-0.0010797185051123));
#29450=CARTESIAN_POINT('',(-0.00205271390416077,0.00440770278012309,-0.0010434426181064));
#29451=CARTESIAN_POINT('',(-0.000694266935139823,0.00481153922800441,-0.000970931729240861));
#29452=CARTESIAN_POINT('',(2.83990257170628E-5,0.00486200363715436,-0.000934831834017371));
#29453=CARTESIAN_POINT('',(0.00143050568294445,0.00464625140692806,-0.000862160801424495));
#29454=CARTESIAN_POINT('',(0.00210442357992056,0.00438274985912574,-0.0008261501038993));
#29455=CARTESIAN_POINT('',(0.00328029438802367,0.00358831224337118,-0.000753425052819996));
#29456=CARTESIAN_POINT('',(0.00377640191472476,0.00306156404473047,-0.000717414577191283));
#29457=CARTESIAN_POINT('',(0.00449985204132285,0.00184128869076413,-0.000644743008267738));
#29458=CARTESIAN_POINT('',(0.00472286519121912,0.00115206824794936,-0.000608643685588099));
#29459=CARTESIAN_POINT('',(0.00485529154939288,-0.000258933233588963,-0.000536131947877782));
#29460=CARTESIAN_POINT('',(0.00476177623805602,-0.000978868713518357,-0.000499856711169238));
#29461=CARTESIAN_POINT('',(0.00427897093691628,-0.00230887730190805,-0.000427607498759415));
#29462=CARTESIAN_POINT('',(0.00388561770330911,-0.0029217373297186,-0.000391073676149546));
#29463=CARTESIAN_POINT('',(0.00288231585962286,-0.00391514436386499,-0.000319182923257227));
#29464=CARTESIAN_POINT('',(0.00226538286521803,-0.00430213287322061,-0.000282648806250469));
#29465=CARTESIAN_POINT('',(0.000930586177031152,-0.00477153857249115,-0.000210400323291803));
#29466=CARTESIAN_POINT('',(0.000209705533412433,-0.00485772598645825,-0.000174124436289757));
#29467=CARTESIAN_POINT('',(-0.00119987733525668,-0.00471096706634371,-0.000101613547421149));
#29468=CARTESIAN_POINT('',(-0.00188684551864319,-0.00448103781072582,-6.55136522011198E-5));
#29469=CARTESIAN_POINT('',(-0.00309965835764556,-0.00374514575299485,7.15738039559136E-6));
#29470=CARTESIAN_POINT('',(-0.00362143963251333,-0.00324380485224829,4.31680779204336E-5));
#29471=CARTESIAN_POINT('',(-0.00440378449139505,-0.00205985392233476,0.00011589312899667));
#29472=CARTESIAN_POINT('',(-0.00466055027259318,-0.0013833499116795,0.000151903604627322));
#29473=CARTESIAN_POINT('',(-0.00486195187646446,2.08898894681251E-5,0.000224575173550102));
#29474=CARTESIAN_POINT('',(-0.00480423591642288,0.000742989987624055,0.000260674496229834));
#29475=CARTESIAN_POINT('',(-0.00438661502827317,0.00209726275005857,0.000333186233940918));
#29476=CARTESIAN_POINT('',(-0.00402471076559106,0.00272660964443439,0.000369461470652192));
#29477=CARTESIAN_POINT('',(-0.00306968457809138,0.00377061576736623,0.000441710683041813));
#29478=CARTESIAN_POINT('',(-0.002471742197528,0.00418629483761571,0.000478244505748111));
#29479=CARTESIAN_POINT('',(-0.00116465174499404,0.0047201362713054,0.000550135258627114));
#29480=CARTESIAN_POINT('',(-0.000446585888841052,0.0048415769991423,0.000586669374733954));
#29481=CARTESIAN_POINT('',(0.000966239234472312,0.00476444673680397,0.00065891785890312));
#29482=CARTESIAN_POINT('',(0.00166522860838972,0.00456820444175427,0.000695193749022433));
#29483=CARTESIAN_POINT('',(0.00291135116219289,0.00389319287949821,0.000767704630734155));
#29484=CARTESIAN_POINT('',(0.00345803687626453,0.00341787461537647,0.000803804518873336));
#29485=CARTESIAN_POINT('',(0.00429691613675843,0.00227387557689792,0.000876475585588987));
#29486=CARTESIAN_POINT('',(0.00458712432903145,0.00161101996494976,0.000912486279229324));
#29487=CARTESIAN_POINT('',(0.00485683838280882,0.000217801624758837,0.000985211191673891));
#29488=CARTESIAN_POINT('',(0.00483517205219748,-0.00050546707194813,0.00102122181326199));
#29489=CARTESIAN_POINT('',(0.00448386339341055,-0.00187988821156079,0.00109389386837081));
#29490=CARTESIAN_POINT('',(0.00415420624873737,-0.00252493262350395,0.00112999223805531));
#29491=CARTESIAN_POINT('',(0.00325011547594119,-0.00361630500354902,0.00120250251618307));
#29492=CARTESIAN_POINT('',(0.0026749141028128,-0.00405925590161076,0.0012387820458946));
#29493=CARTESIAN_POINT('',(0.00139308020350591,-0.00465830042112489,0.00131103488438839));
#29494=CARTESIAN_POINT('',(0.000681577685454135,-0.00481351659471675,0.00134753834547939));
#29495=CARTESIAN_POINT('',(-0.00127951311719603,-0.00480384708244003,0.00144741961858554));
#29496=CARTESIAN_POINT('',(-0.00253526298152253,-0.00427549071008319,0.0015126361106183));
#29497=CARTESIAN_POINT('',(-0.00430219482895177,-0.00249195208003113,0.00164065404675544));
#29498=CARTESIAN_POINT('',(-0.00481625326789864,-0.00121879809522714,0.00170645154026259));
#29499=CARTESIAN_POINT('',(-0.00481005712741422,2.43759101882384E-5,0.00176981449410054));
#29500=CARTESIAN_POINT('',(-0.006,2.43712308653094E-5,-0.0152300713606537));
#29501=CARTESIAN_POINT('',(-0.00599690252296466,0.000804744810155825,-0.0151980803713376));
#29502=CARTESIAN_POINT('',(-0.00583736572769333,0.00159298335532281,-0.0151657322674743));
#29503=CARTESIAN_POINT('',(-0.00485144734603198,0.00395139172205703,-0.0150609128940259));
#29504=CARTESIAN_POINT('',(-0.00341173734068717,0.00524330426742482,-0.0149885940536295));
#29505=CARTESIAN_POINT('',(-0.000871709513217771,0.00600125062263071,-0.0148799265127186));
#29506=CARTESIAN_POINT('',(3.09456231818347E-5,0.00606467923987668,-0.0148437081733647));
#29507=CARTESIAN_POINT('',(0.00177788269483879,0.00579767665572992,-0.0147712652361108));
#29508=CARTESIAN_POINT('',(0.00262079982041912,0.00546892620520059,-0.014735042802557));
#29509=CARTESIAN_POINT('',(0.0040861725105118,0.00448104450356913,-0.0146625997584658));
#29510=CARTESIAN_POINT('',(0.00470725422304886,0.0038231374713461,-0.0146263783962704));
#29511=CARTESIAN_POINT('',(0.00561002149547192,0.00230389862445774,-0.0145539348965588));
#29512=CARTESIAN_POINT('',(0.00588984517702552,0.00144339140566514,-0.0145177135756586));
#29513=CARTESIAN_POINT('',(0.00605673801000797,-0.000315828556998168,-0.0144452699879439));
#29514=CARTESIAN_POINT('',(0.00594161714193286,-0.0012135250192261,-0.0144090487223906));
#29515=CARTESIAN_POINT('',(0.00534034342389439,-0.00287507220515675,-0.014336605167007));
#29516=CARTESIAN_POINT('',(0.00485259831696443,-0.00363767036522909,-0.0143003837319588));
#29517=CARTESIAN_POINT('',(0.00359825268706524,-0.00488212214941821,-0.0142279405377117));
#29518=CARTESIAN_POINT('',(0.00283158196400144,-0.00536350310207911,-0.0141917188067142));
#29519=CARTESIAN_POINT('',(0.00116524705640889,-0.00595137856142856,-0.0141192759847855));
#29520=CARTESIAN_POINT('',(0.000266605506933447,-0.00605917232737577,-0.014083054070165));
#29521=CARTESIAN_POINT('',(-0.00149119555580268,-0.00587794805649581,-0.0140106113143761));
#29522=CARTESIAN_POINT('',(-0.00234945104947196,-0.00559120884671478,-0.0139743894342706));
#29523=CARTESIAN_POINT('',(-0.00386122980401518,-0.00467600158772933,-0.0139019465260691));
#29524=CARTESIAN_POINT('',(-0.00451416703400287,-0.00404968665906797,-0.0138657248191622));
#29525=CARTESIAN_POINT('',(-0.00548995216528817,-0.00257623315922293,-0.0137932816441086));
#29526=CARTESIAN_POINT('',(-0.00581198832858315,-0.00173073160427836,-0.0137570601590698));
#29527=CARTESIAN_POINT('',(-0.00606464765160479,1.83374390645552E-5,-0.0136846167145914));
#29528=CARTESIAN_POINT('',(-0.0059938691252166,0.00092042665972075,-0.0136483954069969));
#29529=CARTESIAN_POINT('',(-0.005474834059304,0.00260960080412937,-0.0135759518024328));
#29530=CARTESIAN_POINT('',(-0.00502494259376194,0.00339490932190728,-0.0135397305379354));
#29531=CARTESIAN_POINT('',(-0.00383359144441473,0.00469988132061323,-0.0134672869867618));
#29532=CARTESIAN_POINT('',(-0.00309114007954832,0.00521777818798231,-0.0134310655505372));
#29533=CARTESIAN_POINT('',(-0.00145604475526128,0.00588748441466296,-0.0133586223554552));
#29534=CARTESIAN_POINT('',(-0.000563516845062604,0.006038830241408,-0.013322400624863));
#29535=CARTESIAN_POINT('',(0.0012009460703243,0.00594427758822637,-0.0132499578030685));
#29536=CARTESIAN_POINT('',(0.00207243349249206,0.00569997080779686,-0.0132137358883429));
#29537=CARTESIAN_POINT('',(0.00362707839031281,0.00485986006847225,-0.0131412931325354));
#29538=CARTESIAN_POINT('',(0.00431027272978388,0.00426650742375495,-0.013105071252456));
#29539=CARTESIAN_POINT('',(0.00535673952363115,0.00284243348643018,-0.0130326283442549));
#29540=CARTESIAN_POINT('',(0.00572029451972927,0.00201392568252568,-0.0129964066373418));
#29541=CARTESIAN_POINT('',(0.00605793618792313,0.000279215348634717,-0.0129239634622906));
#29542=CARTESIAN_POINT('',(0.00603189937079921,-0.000625164136977061,-0.0128877419772535));
#29543=CARTESIAN_POINT('',(0.00559598640309222,-0.00233778176403413,-0.0128152985327716));
#29544=CARTESIAN_POINT('',(0.00518538097196905,-0.00314411776208916,-0.0127790772251792));
#29545=CARTESIAN_POINT('',(0.00405943613844661,-0.00450608506039521,-0.012706633620614));
#29546=CARTESIAN_POINT('',(0.00334326606254171,-0.0050594495164588,-0.0126704123561171));
#29547=CARTESIAN_POINT('',(0.0017432099560226,-0.00580917608958445,-0.0125979688049435));
#29548=CARTESIAN_POINT('',(0.000859083785322923,-0.00600352656862025,-0.012561747368715));
#29549=CARTESIAN_POINT('',(-0.000907832795992274,-0.00599653055331017,-0.0124893041736411));
#29550=CARTESIAN_POINT('',(-0.00179033860487747,-0.00579480022081359,-0.0124530824430416));
#29551=CARTESIAN_POINT('',(-0.00338430604441628,-0.00503221423504633,-0.0123806396212533));
#29552=CARTESIAN_POINT('',(-0.00409596327930432,-0.00447300040297535,-0.0123444177065222));
#29553=CARTESIAN_POINT('',(-0.0052107714194494,-0.00310190244027309,-0.0122719749507197));
#29554=CARTESIAN_POINT('',(-0.00561489445973178,-0.00229226892145074,-0.0122357530706378));
#29555=CARTESIAN_POINT('',(-0.00603673420972488,-0.000576130653447598,-0.0121633101624367));
#29556=CARTESIAN_POINT('',(-0.00605555901945168,0.000328437222868882,-0.0121270884555252));
#29557=CARTESIAN_POINT('',(-0.00570365434124662,0.00206031046766952,-0.012054645280471));
#29558=CARTESIAN_POINT('',(-0.00533350841312408,0.00288588430551408,-0.0120184237954346));
#29559=CARTESIAN_POINT('',(-0.00427538695244329,0.00430132000746911,-0.0119459803509542));
#29560=CARTESIAN_POINT('',(-0.00358746557130879,0.00488914543665951,-0.0119097590433595));
#29561=CARTESIAN_POINT('',(-0.00202602586441541,0.00571655871399608,-0.0118373154387974));
#29562=CARTESIAN_POINT('',(-0.00115260758008782,0.00595373438615169,-0.011801094174299));
#29563=CARTESIAN_POINT('',(0.000612559445933921,0.00603407645922647,-0.0117286506231255));
#29564=CARTESIAN_POINT('',(0.00150376022760004,0.00587529245128564,-0.0116924291869014));
#29565=CARTESIAN_POINT('',(0.00313350103358548,0.00519265927390464,-0.0116199859918183));
#29566=CARTESIAN_POINT('',(0.00387163123167716,0.00466856439659248,-0.0115837642612236));
#29567=CARTESIAN_POINT('',(0.00505243610205558,0.00335404188172309,-0.0115113214394352));
#29568=CARTESIAN_POINT('',(0.00549591978685464,0.00256505623465993,-0.0114750995247055));
#29569=CARTESIAN_POINT('',(0.006001171735723,0.000871708284348305,-0.0114026567689));
#29570=CARTESIAN_POINT('',(0.00606469940733337,-3.09467446789897E-5,-0.0113664348888228));
#29571=CARTESIAN_POINT('',(0.00579769083551663,-0.00177788284887564,-0.0112939919806155));
#29572=CARTESIAN_POINT('',(0.00546891955221835,-0.00262079853837439,-0.011257770273707));
#29573=CARTESIAN_POINT('',(0.00448104282489471,-0.00408617269203305,-0.0111853270986528));
#29574=CARTESIAN_POINT('',(0.00382313914792685,-0.00470725474914973,-0.0111491056136164));
#29575=CARTESIAN_POINT('',(0.002303898594764,-0.00561002127132331,-0.011076662169136));
#29576=CARTESIAN_POINT('',(0.00144339105789126,-0.00588984503873103,-0.0110404408615413));
#29577=CARTESIAN_POINT('',(-0.000315828481518282,-0.00605673812410452,-0.0109679972569792));
#29578=CARTESIAN_POINT('',(-0.00121352495802194,-0.00594161716629411,-0.01093177599248));
#29579=CARTESIAN_POINT('',(-0.00287507222511445,-0.00534034338698825,-0.0108593324413081));
#29580=CARTESIAN_POINT('',(-0.00363767037747606,-0.0048525983178956,-0.0108231110050779));
#29581=CARTESIAN_POINT('',(-0.00488212214408763,-0.00359825269162657,-0.0107506678100055));
#29582=CARTESIAN_POINT('',(-0.00536350309988019,-0.00283158196363093,-0.0107144460794054));
#29583=CARTESIAN_POINT('',(-0.0059513785636077,-0.00116524705637126,-0.010642003257617));
#29584=CARTESIAN_POINT('',(-0.00605917232747766,-0.000266605506908352,-0.0106057813428858));
#29585=CARTESIAN_POINT('',(-0.00587794805600551,0.00149119555581136,-0.0105333385870834));
#29586=CARTESIAN_POINT('',(-0.0055912088468016,0.00234945104947269,-0.0104971167070027));
#29587=CARTESIAN_POINT('',(-0.00467600158780397,0.00386122980400121,-0.0104246737987992));
#29588=CARTESIAN_POINT('',(-0.00404968665904617,0.00451416703401636,-0.0103884520918877));
#29589=CARTESIAN_POINT('',(-0.0025762331591996,0.00548995216527635,-0.0103160089168357));
#29590=CARTESIAN_POINT('',(-0.00173073160428898,0.00581198832858672,-0.0102797874318002));
#29591=CARTESIAN_POINT('',(1.83374390657506E-5,0.00606464765160122,-0.0102073439873159));
#29592=CARTESIAN_POINT('',(0.00092042665972273,0.00599386912521625,-0.0101711226797231));
#29593=CARTESIAN_POINT('',(0.00260960080412948,0.00547483405930433,-0.010098679075161));
#29594=CARTESIAN_POINT('',(0.00339490932190509,0.00502494259375986,-0.0100624578106634));
#29595=CARTESIAN_POINT('',(0.00469988132061564,0.00383359144441648,-0.00999001425948835));
#29596=CARTESIAN_POINT('',(0.00521777818797358,0.00309114007954574,-0.00995379282326351));
#29597=CARTESIAN_POINT('',(0.0058874844146718,0.00145604475526363,-0.00988134962818345));
#29598=CARTESIAN_POINT('',(0.00603883024141418,0.000563516845061795,-0.0098451278975872));
#29599=CARTESIAN_POINT('',(0.00594427758822029,-0.00120094607032303,-0.00977268507579888));
#29600=CARTESIAN_POINT('',(0.00569997080779778,-0.0020724334924908,-0.00973646316106843));
#29601=CARTESIAN_POINT('',(0.00485986006847123,-0.00362707839031427,-0.00966402040526441));
#29602=CARTESIAN_POINT('',(0.00426650742376162,-0.00431027272979533,-0.00962779852518529));
#29603=CARTESIAN_POINT('',(0.00284243348642524,-0.00535673952361845,-0.00955535561698029));
#29604=CARTESIAN_POINT('',(0.00201392568252852,-0.00572029451974243,-0.00951913391007031));
#29605=CARTESIAN_POINT('',(0.000279215348634508,-0.00605793618790945,-0.00944669073501678));
#29606=CARTESIAN_POINT('',(-0.000625164136976053,-0.00603189937080213,-0.00941046924998202));
#29607=CARTESIAN_POINT('',(-0.00233778176403151,-0.00559598640309019,-0.00933802580549774));
#29608=CARTESIAN_POINT('',(-0.00314411776208609,-0.00518538097196428,-0.00930180449790574));
#29609=CARTESIAN_POINT('',(-0.00450608506039847,-0.0040594361384512,-0.00922936089334209));
#29610=CARTESIAN_POINT('',(-0.00505944951645661,-0.00334326606254395,-0.009193139628846));
#29611=CARTESIAN_POINT('',(-0.00580917608958444,-0.00174320995602507,-0.0091206960776694));
#29612=CARTESIAN_POINT('',(-0.00600352656861679,-0.000859083785322946,-0.00908447464143997));
#29613=CARTESIAN_POINT('',(-0.00599653055331361,0.000907832795992958,-0.00901203144637064));
#29614=CARTESIAN_POINT('',(-0.00579480022080864,0.00179033860487189,-0.00897580971576979));
#29615=CARTESIAN_POINT('',(-0.00503221423505353,0.00338430604441708,-0.00890336689397993));
#29616=CARTESIAN_POINT('',(-0.00447300040297218,0.00409596327929867,-0.00886714497924948));
#29617=CARTESIAN_POINT('',(-0.00310190244027584,0.00521077141945543,-0.008794702223447));
#29618=CARTESIAN_POINT('',(-0.0022922689214523,0.00561489445972799,-0.00875848034336713));
#29619=CARTESIAN_POINT('',(-0.00057613065345023,0.00603673420972755,-0.00868603743516212));
#29620=CARTESIAN_POINT('',(0.000328437222867063,0.00605555901944492,-0.00864981572825367));
#29621=CARTESIAN_POINT('',(0.00206031046767124,0.00570365434125339,-0.00857737255319708));
#29622=CARTESIAN_POINT('',(0.00288588430551185,0.00533350841312284,-0.00854115106816231));
#29623=CARTESIAN_POINT('',(0.0043013200074696,0.0042753869524458,-0.00846870762368109));
#29624=CARTESIAN_POINT('',(0.00488914543666715,0.00358746557131492,-0.00843248631608679));
#29625=CARTESIAN_POINT('',(0.00571655871398774,0.00202602586441055,-0.00836004271152468));
#29626=CARTESIAN_POINT('',(0.00595373438615279,0.00115260758008786,-0.00832382144702628));
#29627=CARTESIAN_POINT('',(0.00603407645922529,-0.000612559445933486,-0.00825137789585275));
#29628=CARTESIAN_POINT('',(0.0058752924512829,-0.00150376022759798,-0.00821515645962792));
#29629=CARTESIAN_POINT('',(0.00519265927390726,-0.00313350103358763,-0.00814271326454633));
#29630=CARTESIAN_POINT('',(0.00466856439658982,-0.00387163123167595,-0.00810649153395315));
#29631=CARTESIAN_POINT('',(0.00335404188172599,-0.0050524361020565,-0.00803404871216023));
#29632=CARTESIAN_POINT('',(0.002565056234659,-0.00549591978684913,-0.00799782679743132));
#29633=CARTESIAN_POINT('',(0.000871708284350316,-0.00600117173572815,-0.00792538404162886));
#29634=CARTESIAN_POINT('',(-3.09467446757314E-5,-0.00606469940732576,-0.0078891621615482));
#29635=CARTESIAN_POINT('',(-0.00177788284887691,-0.0057976908355244,-0.00781671925334474));
#29636=CARTESIAN_POINT('',(-0.00262079853836913,-0.00546891955220997,-0.00778049754643241));
#29637=CARTESIAN_POINT('',(-0.0040861726920387,-0.0044810428249027,-0.00770805437138196));
#29638=CARTESIAN_POINT('',(-0.00470725474913832,-0.00382313914792043,-0.00767183288634381));
#29639=CARTESIAN_POINT('',(-0.00561002127133291,-0.00230389859477328,-0.00759938944186337));
#29640=CARTESIAN_POINT('',(-0.00588984503872023,-0.00144339105788938,-0.00756316813426977));
#29641=CARTESIAN_POINT('',(-0.00605673812411518,0.000315828481515877,-0.00749072452970536));
#29642=CARTESIAN_POINT('',(-0.00594161716629604,0.0012135249580206,-0.0074545032652082));
#29643=CARTESIAN_POINT('',(-0.00534034338698797,0.00287507222511094,-0.00738205971403469));
#29644=CARTESIAN_POINT('',(-0.00485259831790225,0.00363767037748548,-0.00734583827780744));
#29645=CARTESIAN_POINT('',(-0.00359825269161942,0.00488212214407865,-0.00727339508273044));
#29646=CARTESIAN_POINT('',(-0.00283158196363257,0.005363503099875,-0.00723717335213202));
#29647=CARTESIAN_POINT('',(-0.00116524705637457,0.00595137856361104,-0.00716473053034522));
#29648=CARTESIAN_POINT('',(-0.000266605506907021,0.00605917232748146,-0.00712850861561236));
#29649=CARTESIAN_POINT('',(0.00149119555581047,0.00587794805600161,-0.0070560658598114));
#29650=CARTESIAN_POINT('',(0.00234945104945872,0.00559120884678573,-0.0070198439797293));
#29651=CARTESIAN_POINT('',(0.00386122980401202,0.00467600158782171,-0.00694740107152736));
#29652=CARTESIAN_POINT('',(0.0045141670340063,0.00404968665904241,-0.00691117936461584));
#29653=CARTESIAN_POINT('',(0.00548995216528485,0.00257623315920559,-0.0068387361895623));
#29654=CARTESIAN_POINT('',(0.00581198832858654,0.00173073160428969,-0.00680251470452446));
#29655=CARTESIAN_POINT('',(0.00606464765160107,-1.83374390644384E-5,-0.0067300712600463));
#29656=CARTESIAN_POINT('',(0.00599386912521984,-0.000920426659723841,-0.00669384995245127));
#29657=CARTESIAN_POINT('',(0.00547483405930049,-0.00260960080412893,-0.00662140634788747));
#29658=CARTESIAN_POINT('',(0.00502494259376497,-0.00339490932190835,-0.0065851850833907));
#29659=CARTESIAN_POINT('',(0.00383359144441144,-0.00469988132061221,-0.00651274153221563));
#29660=CARTESIAN_POINT('',(0.00309114007954164,-0.00521777818796783,-0.00647652009599003));
#29661=CARTESIAN_POINT('',(0.00145604475526746,-0.00588748441467761,-0.0064040769009115));
#29662=CARTESIAN_POINT('',(0.000563516845063924,-0.00603883024140614,-0.00636785517031527));
#29663=CARTESIAN_POINT('',(-0.00120094607032435,-0.00594427758822836,-0.00629541234852541));
#29664=CARTESIAN_POINT('',(-0.00207243349248784,-0.00569997080779289,-0.00625919043379578));
#29665=CARTESIAN_POINT('',(-0.0036270783903172,-0.00485986006847613,-0.00618674767799164));
#29666=CARTESIAN_POINT('',(-0.0043102727297894,-0.00426650742375841,-0.0061505257979118));
#29667=CARTESIAN_POINT('',(-0.0053567395236248,-0.00284243348642777,-0.00607808288970833));
#29668=CARTESIAN_POINT('',(-0.00572029451974054,-0.00201392568252749,-0.00604186118279835));
#29669=CARTESIAN_POINT('',(-0.0060579361879114,-0.000279215348635194,-0.00596941800774329));
#29670=CARTESIAN_POINT('',(-0.00603189937080701,0.000625164136977491,-0.00593319652270699));
#29671=CARTESIAN_POINT('',(-0.0055959864030851,0.00233778176403084,-0.00586075307822731));
#29672=CARTESIAN_POINT('',(-0.00518538097195793,0.00314411776208208,-0.00582453177063385));
#29673=CARTESIAN_POINT('',(-0.00405943613845727,0.00450608506040282,-0.00575208816606853));
#29674=CARTESIAN_POINT('',(-0.00334326606254177,0.00505944951645318,-0.00571586690157174));
#29675=CARTESIAN_POINT('',(-0.00174320995602712,0.00580917608958792,-0.00564342335039822));
#29676=CARTESIAN_POINT('',(-0.000859083785322943,0.00600352656860298,-0.00560720191417491));
#29677=CARTESIAN_POINT('',(0.000907832795993349,0.00599653055332741,-0.00553475871909025));
#29678=CARTESIAN_POINT('',(0.00179033860487224,0.00579480022080926,-0.00549853698849628));
#29679=CARTESIAN_POINT('',(0.00338430604441741,0.00503221423505262,-0.00542609416670796));
#29680=CARTESIAN_POINT('',(0.00409596327930708,0.00447300040297686,-0.00538987225197682));
#29681=CARTESIAN_POINT('',(0.00521077141944732,0.00310190244027081,-0.00531742949617421));
#29682=CARTESIAN_POINT('',(0.00561489445973345,0.00229226892145273,-0.00528120761609439));
#29683=CARTESIAN_POINT('',(0.00603673420972227,0.000576130653449121,-0.00520876470788938));
#29684=CARTESIAN_POINT('',(0.00605555901943846,-0.000328437222866894,-0.00517254300097944));
#29685=CARTESIAN_POINT('',(0.00570365434125996,-0.00206031046767069,-0.00510009982592591));
#29686=CARTESIAN_POINT('',(0.0053335084131272,-0.00288588430551483,-0.00506387834089111));
#29687=CARTESIAN_POINT('',(0.00427538695244096,-0.0043013200074672,-0.00499143489640682));
#29688=CARTESIAN_POINT('',(0.0035874655713107,-0.00488914543666087,-0.00495521358881489));
#29689=CARTESIAN_POINT('',(0.0020260258644141,-0.00571655871399437,-0.00488276998425111));
#29690=CARTESIAN_POINT('',(0.00115260758008779,-0.0059537343861532,-0.00484654871975433));
#29691=CARTESIAN_POINT('',(-0.000612559445933405,-0.00603407645922492,-0.00477410516857927));
#29692=CARTESIAN_POINT('',(-0.00150376022759912,-0.00587529245128513,-0.00473788373235367));
#29693=CARTESIAN_POINT('',(-0.00313350103358697,-0.00519265927390485,-0.00466544053727514));
#29694=CARTESIAN_POINT('',(-0.0038716312316762,-0.0046685643965911,-0.00462921880667965));
#29695=CARTESIAN_POINT('',(-0.00505243610205692,-0.00335404188172401,-0.00455677598488826));
#29696=CARTESIAN_POINT('',(-0.00549591978685125,-0.00256505623465877,-0.00452055407015787));
#29697=CARTESIAN_POINT('',(-0.00600117173572664,-0.000871708284348603,-0.0044481113143568));
#29698=CARTESIAN_POINT('',(-0.00606469940732523,3.09467446769893E-5,-0.00441188943427621));
#29699=CARTESIAN_POINT('',(-0.0057976908355246,0.00177788284887812,-0.00433944652607121));
#29700=CARTESIAN_POINT('',(-0.00546891955221376,0.00262079853837175,-0.00430322481915968));
#29701=CARTESIAN_POINT('',(-0.00448104282489869,0.00408617269203654,-0.00423078164410923));
#29702=CARTESIAN_POINT('',(-0.00382313914792086,0.00470725474914317,-0.0041945601590714));
#29703=CARTESIAN_POINT('',(-0.00230389859476928,0.00561002127133021,-0.00412211671459019));
#29704=CARTESIAN_POINT('',(-0.00144339105789001,0.0058898450387264,-0.00408589540699673));
#29705=CARTESIAN_POINT('',(0.000315828481517189,0.00605673812410911,-0.00401345180243295));
#29706=CARTESIAN_POINT('',(0.0012135249580228,0.00594161716629725,-0.0039772305379354));
#29707=CARTESIAN_POINT('',(0.002875072225113,0.00534034338698525,-0.00390478698676188));
#29708=CARTESIAN_POINT('',(0.00363767037748591,0.00485259831790412,-0.00386856555053472));
#29709=CARTESIAN_POINT('',(0.00488212214407839,0.00359825269161736,-0.00379612235545772));
#29710=CARTESIAN_POINT('',(0.00536350309987848,0.00283158196362959,-0.00375990062486069));
#29711=CARTESIAN_POINT('',(0.00595137856360991,0.00116524705637084,-0.00368745780307082));
#29712=CARTESIAN_POINT('',(0.00605917232748467,0.000266605506905886,-0.00365123588834047));
#29713=CARTESIAN_POINT('',(0.00587794805599835,-0.00149119555580979,-0.00357879313253784));
#29714=CARTESIAN_POINT('',(0.0055912088467858,-0.00234945104946311,-0.00354257125245874));
#29715=CARTESIAN_POINT('',(0.00467600158781796,-0.00386122980401372,-0.00347012834425219));
#29716=CARTESIAN_POINT('',(0.00404968665903719,-0.00451416703400542,-0.00343390663734299));
#29717=CARTESIAN_POINT('',(0.00257623315920537,-0.00548995216528933,-0.00336146346228945));
#29718=CARTESIAN_POINT('',(0.00173073160428629,-0.00581198832858667,-0.0033252419772539));
#29719=CARTESIAN_POINT('',(-1.83374390680346E-5,-0.00606464765160196,-0.00325279853277114));
#29720=CARTESIAN_POINT('',(-0.000920426659724022,-0.00599386912522055,-0.00321657722517854));
#29721=CARTESIAN_POINT('',(-0.00260960080412909,-0.00547483405929967,-0.00314413362061474));
#29722=CARTESIAN_POINT('',(-0.00339490932190975,-0.00502494259376035,-0.00310791235611861));
#29723=CARTESIAN_POINT('',(-0.00469988132061588,-0.00383359144441144,-0.00303546880494201));
#29724=CARTESIAN_POINT('',(-0.00521777818796983,-0.00309114007954222,-0.00299924736871654));
#29725=CARTESIAN_POINT('',(-0.00588748441467571,-0.00145604475526665,-0.00292680417363955));
#29726=CARTESIAN_POINT('',(-0.00603883024140671,-0.000563516845059997,-0.00289058244304164));
#29727=CARTESIAN_POINT('',(-0.00594427758822741,0.00120094607032737,-0.00281813962125333));
#29728=CARTESIAN_POINT('',(-0.00569997080779323,0.00207243349248791,-0.00278191770652306));
#29729=CARTESIAN_POINT('',(-0.00485986006847584,0.00362707839031703,-0.00270947495071892));
#29730=CARTESIAN_POINT('',(-0.00426650742375889,0.00431027272979482,-0.002673253070639));
#29731=CARTESIAN_POINT('',(-0.00284243348642429,0.00535673952362161,-0.00260081016243554));
#29732=CARTESIAN_POINT('',(-0.00201392568252745,0.00572029451974175,-0.00256458845552562));
#29733=CARTESIAN_POINT('',(-0.000279215348634867,0.00605793618791026,-0.00249214528047057));
#29734=CARTESIAN_POINT('',(0.00062516413697907,0.00603189937080894,-0.0024559237954365));
#29735=CARTESIAN_POINT('',(0.00233778176403195,0.00559598640308249,-0.00238348035095223));
#29736=CARTESIAN_POINT('',(0.00314411776208378,0.00518538097195793,-0.00234725904336031));
#29737=CARTESIAN_POINT('',(0.00450608506040276,0.00405943613845593,-0.00227481543879654));
#29738=CARTESIAN_POINT('',(0.0050594495164604,0.00334326606254532,-0.002238594174299));
#29739=CARTESIAN_POINT('',(0.00580917608958121,0.00174320995602248,-0.00216615062312549));
#29740=CARTESIAN_POINT('',(0.00600352656860681,0.000859083785322374,-0.00212992918689912));
#29741=CARTESIAN_POINT('',(0.00599653055332356,-0.000907832795993293,-0.00205748599182059));
#29742=CARTESIAN_POINT('',(0.00579480022080894,-0.00179033860487247,-0.00202126426122357));
#29743=CARTESIAN_POINT('',(0.00503221423505307,-0.00338430604441687,-0.00194882143943525));
#29744=CARTESIAN_POINT('',(0.00447300040297654,-0.00409596327930717,-0.00191259952470409));
#29745=CARTESIAN_POINT('',(0.00310190244027087,-0.00521077141944741,-0.00184015676890149));
#29746=CARTESIAN_POINT('',(0.00229226892145273,-0.00561489445973389,-0.0018039348888209));
#29747=CARTESIAN_POINT('',(0.000576130653448751,-0.00603673420972194,-0.00173149198061743));
#29748=CARTESIAN_POINT('',(-0.000328437222867711,-0.00605555901944176,-0.00169527027370514));
#29749=CARTESIAN_POINT('',(-0.00206031046767129,-0.00570365434125637,-0.00162282709865468));
#29750=CARTESIAN_POINT('',(-0.00288588430551477,-0.00533350841312699,-0.00158660561361686));
#29751=CARTESIAN_POINT('',(-0.00430132000746675,-0.00427538695244153,-0.00151416216913565));
#29752=CARTESIAN_POINT('',(-0.00488914543666364,-0.00358746557131148,-0.00147794086154216));
#29753=CARTESIAN_POINT('',(-0.00571655871399177,-0.00202602586441296,-0.00140549725697838));
#29754=CARTESIAN_POINT('',(-0.00595373438615588,-0.00115260758008819,-0.00136927599248006));
#29755=CARTESIAN_POINT('',(-0.00603407645922224,0.000612559445934199,-0.00129683244130807));
#29756=CARTESIAN_POINT('',(-0.00587529245128122,0.00150376022759815,-0.0012606110050794));
#29757=CARTESIAN_POINT('',(-0.00519265927390861,0.0031335010335883,-0.00118816781000394));
#29758=CARTESIAN_POINT('',(-0.00466856439659019,0.00387163123167518,-0.00115194607940538));
#29759=CARTESIAN_POINT('',(-0.00335404188172464,0.00505243610205819,-0.00107950325761706));
#29760=CARTESIAN_POINT('',(-0.00256505623465843,0.00549591978684937,-0.00104328134288591));
#29761=CARTESIAN_POINT('',(-0.000871708284348645,0.00600117173572859,-0.000970838587083295));
#29762=CARTESIAN_POINT('',(3.09467446766596E-5,0.0060646994073229,-0.000934616707003476));
#29763=CARTESIAN_POINT('',(0.00177788284887884,0.00579769083552687,-0.000862173798798473));
#29764=CARTESIAN_POINT('',(0.00262079853837167,0.00546891955221328,-0.000825952091889253));
#29765=CARTESIAN_POINT('',(0.00408617269203685,0.00448104282489897,-0.00075350891683419));
#29766=CARTESIAN_POINT('',(0.00470725474914363,0.00382313914792303,-0.000717287431798667));
#29767=CARTESIAN_POINT('',(0.00561002127132991,0.00230389859476685,-0.000644843987317453));
#29768=CARTESIAN_POINT('',(0.00588984503872567,0.00144339105788941,-0.000608622679723984));
#29769=CARTESIAN_POINT('',(0.00605673812410992,-0.000315828481517504,-0.0005361790751602));
#29770=CARTESIAN_POINT('',(0.00594161716629623,-0.00121352495802331,-0.000499957810662642));
#29771=CARTESIAN_POINT('',(0.00534034338698577,-0.00287507222511389,-0.000427514259489119));
#29772=CARTESIAN_POINT('',(0.00485259831790474,-0.00363767037748681,-0.000391292823261212));
#29773=CARTESIAN_POINT('',(0.00359825269161654,-0.00488212214407767,-0.000318849628185754));
#29774=CARTESIAN_POINT('',(0.00283158196363021,-0.00536350309988268,-0.000282627897588721));
#29775=CARTESIAN_POINT('',(0.00116524705637054,-0.00595137856360559,-0.000210185075797331));
#29776=CARTESIAN_POINT('',(0.000266605506906044,-0.00605917232748427,-0.000173963161068493));
#29777=CARTESIAN_POINT('',(-0.00149119555581014,-0.00587794805599875,-0.000101520405264349));
#29778=CARTESIAN_POINT('',(-0.00234945104946307,-0.00559120884678631,-6.52985251845243E-5));
#29779=CARTESIAN_POINT('',(-0.00386122980401153,-0.0046760015878186,7.14438301894512E-6));
#29780=CARTESIAN_POINT('',(-0.00451416703400858,-0.00404968665904013,4.33660899304402E-5));
#29781=CARTESIAN_POINT('',(-0.00548995216528468,-0.00257623315920546,0.000115809264982434));
#29782=CARTESIAN_POINT('',(-0.00581198832858678,-0.00173073160428641,0.000152030750019587));
#29783=CARTESIAN_POINT('',(-0.00606464765160127,1.83374390675391E-5,0.000224474194500801));
#29784=CARTESIAN_POINT('',(-0.00599386912521991,0.000920426659714502,0.000260695502093955));
#29785=CARTESIAN_POINT('',(-0.00547483405929987,0.00260960080412699,0.000333139106657739));
#29786=CARTESIAN_POINT('',(-0.00502494259376105,0.0033949093219533,0.000369360371157798));
#29787=CARTESIAN_POINT('',(-0.00383359144441966,0.00469988132060065,0.000441803922327982));
#29788=CARTESIAN_POINT('',(-0.00309114007952168,0.00521777818772337,0.000478025358548409));
#29789=CARTESIAN_POINT('',(-0.00145604475525611,0.00588748441486752,0.000550468553641278));
#29790=CARTESIAN_POINT('',(-0.000563516845067593,0.00603883024251221,0.000586690284260184));
#29791=CARTESIAN_POINT('',(0.00120094607027949,0.00594427758669178,0.000659133105962878));
#29792=CARTESIAN_POINT('',(0.00207243349184227,0.00569997080483151,0.000695355020696328));
#29793=CARTESIAN_POINT('',(0.0036270783914194,0.00485986007638553,0.000767797776819668));
#29794=CARTESIAN_POINT('',(0.00431027273332751,0.0042665074258414,0.000804019656535012));
#29795=CARTESIAN_POINT('',(0.00535673951349427,0.00284243345423534,0.000876462563765694));
#29796=CARTESIAN_POINT('',(0.00572029451211937,0.00201392571479105,0.000912684273444742));
#29797=CARTESIAN_POINT('',(0.00605793624792242,0.000279215448155177,0.0009851274504376));
#29798=CARTESIAN_POINT('',(0.0060318993545859,-0.000625164387659044,0.00102134892034041));
#29799=CARTESIAN_POINT('',(0.0055959861469186,-0.00233778194385103,0.00109379236698234));
#29800=CARTESIAN_POINT('',(0.00518538116262535,-0.00314411648770142,0.00113001374476538));
#29801=CARTESIAN_POINT('',(0.00405943692929677,-0.00450608539393174,0.00120245729547706));
#29802=CARTESIAN_POINT('',(0.00334326536337128,-0.00505945513492329,0.00123867827021172));
#29803=CARTESIAN_POINT('',(0.00174320839046504,-0.00580917059968966,0.00131112223223615));
#29804=CARTESIAN_POINT('',(0.000859084702433251,-0.00600351044798021,0.00134734474006646));
#29805=CARTESIAN_POINT('',(-0.00159496641848697,-0.00599385800234282,0.00144795686576414));
#29806=CARTESIAN_POINT('',(-0.00315377058881324,-0.00533975389994977,0.00151238270347832));
#29807=CARTESIAN_POINT('',(-0.00536605961859909,-0.00311114458504296,0.0016411109293347));
#29808=CARTESIAN_POINT('',(-0.00600625207018257,-0.00153637595212074,0.00170594725770846));
#29809=CARTESIAN_POINT('',(-0.00600005712193031,2.43712307539645E-5,0.00176992864208601));
#29810=CARTESIAN_POINT('',(-0.00719,2.43712308653001E-5,-0.0152300713606537));
#29811=CARTESIAN_POINT('',(-0.00718690252158388,0.000963531398886715,-0.0151977711561101));
#29812=CARTESIAN_POINT('',(-0.0069976071514561,0.00190126501000997,-0.0151659831835772));
#29813=CARTESIAN_POINT('',(-0.00581496217549105,0.00473548102193302,-0.0150600404237794));
#29814=CARTESIAN_POINT('',(-0.00409179418652758,0.00628072180483626,-0.0149883589919571));
#29815=CARTESIAN_POINT('',(-0.00104907375728438,0.0071909123572038,-0.0148798167218509));
#29816=CARTESIAN_POINT('',(3.35199355820819E-5,0.0072673711660381,-0.0148435071276401));
#29817=CARTESIAN_POINT('',(0.00212523469640938,0.00694911971731699,-0.0147712812165734));
#29818=CARTESIAN_POINT('',(0.00313717278285731,0.0065550974911468,-0.0147348400891705));
#29819=CARTESIAN_POINT('',(0.00489205526552821,0.00537377185160928,-0.0146626838737225));
#29820=CARTESIAN_POINT('',(0.00563810694958756,0.00458471263506918,-0.0146262525303834));
#29821=CARTESIAN_POINT('',(0.00672019040191557,0.00276650918727105,-0.0145540354134981));
#29822=CARTESIAN_POINT('',(0.00705682503309421,0.00173471416688417,-0.0145176922841528));
#29823=CARTESIAN_POINT('',(0.00725818458114715,-0.000372723806555423,-0.0144453173457367));
#29824=CARTESIAN_POINT('',(0.00712145806485822,-0.00144818128856786,-0.0144091498714224));
#29825=CARTESIAN_POINT('',(0.00640171586403277,-0.00344126714619258,-0.0143365118456955));
#29826=CARTESIAN_POINT('',(0.00581957894570077,-0.0043536033968103,-0.0143006028835282));
#29827=CARTESIAN_POINT('',(0.00431418951861804,-0.00584909993211931,-0.0142276072565402));
#29828=CARTESIAN_POINT('',(0.00339778105700325,-0.00642487333100277,-0.0141916978952334));
#29829=CARTESIAN_POINT('',(0.00139990793722036,-0.00713121855168838,-0.0141190607367982));
#29830=CARTESIAN_POINT('',(0.000323505481587939,-0.00726061866847718,-0.0140828927954176));
#29831=CARTESIAN_POINT('',(-0.00178251377698793,-0.0070449290461279,-0.0140105181722345));
#29832=CARTESIAN_POINT('',(-0.0028120565804278,-0.00670137988269372,-0.0139741743072064));
#29833=CARTESIAN_POINT('',(-0.00462280125024691,-0.00560685742263364,-0.0139019595234403));
#29834=CARTESIAN_POINT('',(-0.00540689443549387,-0.00485556846586822,-0.0138655268071655));
#29835=CARTESIAN_POINT('',(-0.00657611983919041,-0.00309261239607272,-0.0137933655081125));
#29836=CARTESIAN_POINT('',(-0.0069634263845761,-0.00207811329688733,-0.013756933013686));
#29837=CARTESIAN_POINT('',(-0.00726734342674198,1.57849886640124E-5,-0.0136847176936322));
#29838=CARTESIAN_POINT('',(-0.00718350233401541,0.00109786333180735,-0.0136483744011382));
#29839=CARTESIAN_POINT('',(-0.00656305309032847,0.0031219388582032,-0.0135759989297099));
#29840=CARTESIAN_POINT('',(-0.00602517442190881,0.00406320899944549,-0.0135398316374257));
#29841=CARTESIAN_POINT('',(-0.00459749831080525,0.00562914687378522,-0.0134671937474946));
#29842=CARTESIAN_POINT('',(-0.00371053796164551,0.00624926153808826,-0.0134312846976163));
#29843=CARTESIAN_POINT('',(-0.00174743776495843,0.00705483255841795,-0.0133582890604163));
#29844=CARTESIAN_POINT('',(-0.000680447802063153,0.00723608348462041,-0.0133223797161986));
#29845=CARTESIAN_POINT('',(0.00143565290426297,0.0071241084384027,-0.0132497425555768));
#29846=CARTESIAN_POINT('',(0.00247963838116558,0.00683173716884005,-0.0132135746131063));
#29847=CARTESIAN_POINT('',(0.00434280562235721,0.00582652726309188,-0.0131411999903939));
#29848=CARTESIAN_POINT('',(0.0051625085739271,0.00511514024919255,-0.0131048561254624));
#29849=CARTESIAN_POINT('',(0.0064165629013809,0.00341099136485625,-0.0130326413416085));
#29850=CARTESIAN_POINT('',(0.00685346470998661,0.00241683140327179,-0.012996208625354));
#29851=CARTESIAN_POINT('',(0.00725903404947283,0.000340629183026168,-0.0129240473262826));
#29852=CARTESIAN_POINT('',(0.00722862664215364,-0.000744861568632379,-0.0128876148318792));
#29853=CARTESIAN_POINT('',(0.00670810919405929,-0.00279567535467164,-0.0128153995118028));
#29854=CARTESIAN_POINT('',(0.00621655667007348,-0.00376330079134388,-0.0127790562192913));
#29855=CARTESIAN_POINT('',(0.00486875614303342,-0.00539586709624065,-0.0127066807479202));
#29856=CARTESIAN_POINT('',(0.00401161256188436,-0.00605965005927627,-0.0126705134556151));
#29857=CARTESIAN_POINT('',(0.00209335334315847,-0.00696004001606565,-0.0125978755656686));
#29858=CARTESIAN_POINT('',(0.0010366012222284,-0.00719352623142796,-0.0125619665158032));
#29859=CARTESIAN_POINT('',(-0.00108534555283455,-0.00718653088776051,-0.0124889708785929));
#29860=CARTESIAN_POINT('',(-0.00214047746751151,-0.00694566552742465,-0.0124530615343699));
#29861=CARTESIAN_POINT('',(-0.00405264860378823,-0.00603241739253837,-0.0123804243737688));
#29862=CARTESIAN_POINT('',(-0.004905279777168,-0.00536278561505436,-0.0123442564313078));
#29863=CARTESIAN_POINT('',(-0.00624194467998763,-0.00372108952233651,-0.012271881808556));
#29864=CARTESIAN_POINT('',(-0.00672701543546455,-0.00275016688146852,-0.0122355379436288));
#29865=CARTESIAN_POINT('',(-0.007233461016919,-0.000695832792475087,-0.0121633231598056));
#29866=CARTESIAN_POINT('',(-0.0072566571092172,0.000389846331801014,-0.0121268904434963));
#29867=CARTESIAN_POINT('',(-0.00683682612901503,0.00246321173532615,-0.0120547291445039));
#29868=CARTESIAN_POINT('',(-0.00639333402113541,0.00345443801252094,-0.0120182966500488));
#29869=CARTESIAN_POINT('',(-0.0051276261457341,0.00514994949078618,-0.0119460813299969));
#29870=CARTESIAN_POINT('',(-0.00430319660631132,0.00585580981978926,-0.0119097380375061));
#29871=CARTESIAN_POINT('',(-0.00243323520837243,0.00684832348254616,-0.011837362566069));
#29872=CARTESIAN_POINT('',(-0.00138731905467814,0.00713356432844445,-0.0118011952738008));
#29873=CARTESIAN_POINT('',(0.000729485694685875,0.00723133015881769,-0.0117285573838467));
#29874=CARTESIAN_POINT('',(0.00179514865645682,0.00704264176550971,-0.0116926483340046));
#29875=CARTESIAN_POINT('',(0.00375289484889381,0.0062241450355068,-0.0116196526967552));
#29876=CARTESIAN_POINT('',(0.00463553444612515,0.00559783295629068,-0.0115837433525595));
#29877=CARTESIAN_POINT('',(0.00605266529073645,0.00402234548266771,-0.011511106191943));
#29878=CARTESIAN_POINT('',(0.00658413679358073,0.00307739856515859,-0.0114749382494755));
#29879=CARTESIAN_POINT('',(0.00719080424344732,0.00104914963355636,-0.011402563626752));
#29880=CARTESIAN_POINT('',(0.00726739517750182,-3.34944636365538E-5,-0.0113662197617896));
#29881=CARTESIAN_POINT('',(0.00694913026411556,-0.00212526001481188,-0.0112940049780086));
#29882=CARTESIAN_POINT('',(0.00655508924530735,-0.00313717349682351,-0.0112575722616862));
#29883=CARTESIAN_POINT('',(0.0053737734064212,-0.004892050996048,-0.0111854109626777));
#29884=CARTESIAN_POINT('',(0.00458471425112067,-0.00563810758356804,-0.0111489784682096));
#29885=CARTESIAN_POINT('',(0.00276650849876566,-0.00672019050133081,-0.0110767631481999));
#29886=CARTESIAN_POINT('',(0.00173471386783323,-0.00705682488623721,-0.0110404198556641));
#29887=CARTESIAN_POINT('',(-0.000372723729448532,-0.00725818469882193,-0.0109680443842746));
#29888=CARTESIAN_POINT('',(-0.00144818120252657,-0.00712145809453435,-0.010931877091978));
#29889=CARTESIAN_POINT('',(-0.00344126714832045,-0.00640171583705778,-0.0108592392020331));
#29890=CARTESIAN_POINT('',(-0.00435360342524517,-0.00581957893249035,-0.0108233301522186));
#29891=CARTESIAN_POINT('',(-0.00584909992429929,-0.00431418952362129,-0.0107503345149048));
#29892=CARTESIAN_POINT('',(-0.00642487332654239,-0.0033977810620425,-0.0107144251707447));
#29893=CARTESIAN_POINT('',(-0.00713121855472189,-0.00139990793571158,-0.0106417880101213));
#29894=CARTESIAN_POINT('',(-0.00726061866850349,-0.000323505480401984,-0.0106056200676768));
#29895=CARTESIAN_POINT('',(-0.00704492904566077,0.00178251377636469,-0.0105332454449142));
#29896=CARTESIAN_POINT('',(-0.00670137988286316,0.00281205658029061,-0.0104969015799504));
#29897=CARTESIAN_POINT('',(-0.00560685742262686,0.00462280125036886,-0.0104246867962115));
#29898=CARTESIAN_POINT('',(-0.00485556846583809,0.00540689443551145,-0.0103882540798553));
#29899=CARTESIAN_POINT('',(-0.00309261239607019,0.00657611983916619,-0.0103160927808721));
#29900=CARTESIAN_POINT('',(-0.00207811329689743,0.00696342638457955,-0.0102796602864091));
#29901=CARTESIAN_POINT('',(1.57849886665503E-5,0.00726734342673879,-0.0102074449663641));
#29902=CARTESIAN_POINT('',(0.00109786333180936,0.00718350233401516,-0.0101711016738655));
#29903=CARTESIAN_POINT('',(0.00312193885820439,0.00656305309032835,-0.0100987262024368));
#29904=CARTESIAN_POINT('',(0.00406320899944281,0.00602517442190682,-0.0100625589101613));
#29905=CARTESIAN_POINT('',(0.00562914687378771,0.00459749831080728,-0.00998992102021339));
#29906=CARTESIAN_POINT('',(0.00624926153807862,0.00371053796164257,-0.00995401197036094));
#29907=CARTESIAN_POINT('',(0.00705483255842778,0.0017474377649609,-0.00988101633312613));
#29908=CARTESIAN_POINT('',(0.00723608348462659,0.000680447802062776,-0.00984510698891086));
#29909=CARTESIAN_POINT('',(0.00712410843839661,-0.00143565290426201,-0.00977246982831896));
#29910=CARTESIAN_POINT('',(0.00683173716884047,-0.00247963838116534,-0.00973630188583411));
#29911=CARTESIAN_POINT('',(0.00582652726309132,-0.00434280562235769,-0.00966392726312063));
#29912=CARTESIAN_POINT('',(0.00511514024919991,-0.0051625085739379,-0.00962758339816522));
#29913=CARTESIAN_POINT('',(0.00341099136485094,-0.00641656290136858,-0.00955536861436036));
#29914=CARTESIAN_POINT('',(0.00241683140327399,-0.00685346470999972,-0.00951893589805603));
#29915=CARTESIAN_POINT('',(0.000340629183027104,-0.00725903404945911,-0.00944677459903517));
#29916=CARTESIAN_POINT('',(-0.000744861568630721,-0.00722862664215674,-0.00941034210460012));
#29917=CARTESIAN_POINT('',(-0.00279567535466896,-0.00670810919405725,-0.00933812678453669));
#29918=CARTESIAN_POINT('',(-0.003763300791342,-0.00621655667006781,-0.00930178349202818));
#29919=CARTESIAN_POINT('',(-0.00539586709624276,-0.00486875614303888,-0.00922940802063791));
#29920=CARTESIAN_POINT('',(-0.00605965005927444,-0.0040116125618859,-0.00919324072834359));
#29921=CARTESIAN_POINT('',(-0.00696004001606482,-0.00209335334316259,-0.00912060283839487));
#29922=CARTESIAN_POINT('',(-0.00719352623142277,-0.00103660122222813,-0.00908469378853435));
#29923=CARTESIAN_POINT('',(-0.00718653088776567,0.00108534555283507,-0.00901169815131639));
#29924=CARTESIAN_POINT('',(-0.00694566552741994,0.00214047746750466,-0.00897578880710958));
#29925=CARTESIAN_POINT('',(-0.00603241739254579,0.00405264860378935,-0.00890315164648391));
#29926=CARTESIAN_POINT('',(-0.00536278561505002,0.00490527977716321,-0.00886698370404469));
#29927=CARTESIAN_POINT('',(-0.00372108952234035,0.00624194467999285,-0.00879460908127369));
#29928=CARTESIAN_POINT('',(-0.00275016688147031,0.00672701543546056,-0.00875826521636245));
#29929=CARTESIAN_POINT('',(-0.000695832792478314,0.00723346101692167,-0.0086860504325269));
#29930=CARTESIAN_POINT('',(0.000389846331799902,0.00725665710921006,-0.00864961771623937));
#29931=CARTESIAN_POINT('',(0.00246321173532715,0.00683682612902217,-0.00857745641721546));
#29932=CARTESIAN_POINT('',(0.00345443801251805,0.00639333402113446,-0.0085410239227796));
#29933=CARTESIAN_POINT('',(0.00514994949078697,0.00512762614573659,-0.00846880860272078));
#29934=CARTESIAN_POINT('',(0.00585580981979626,0.00430319660631894,-0.00843246531021346));
#29935=CARTESIAN_POINT('',(0.00684832348253835,0.00243323520836634,-0.00836008983881627));
#29936=CARTESIAN_POINT('',(0.00713356432844592,0.00138731905467778,-0.0083239225465243));
#29937=CARTESIAN_POINT('',(0.00723133015881612,-0.000729485694684936,-0.00825128465657788));
#29938=CARTESIAN_POINT('',(0.00704264176550677,-0.0017951486564551,-0.00821537560673844));
#29939=CARTESIAN_POINT('',(0.00622414503550962,-0.00375289484889564,-0.00814237996947601));
#29940=CARTESIAN_POINT('',(0.00559783295628793,-0.00463553444612385,-0.00810647062529255));
#29941=CARTESIAN_POINT('',(0.00402234548267076,-0.00605266529073742,-0.00803383346466462));
#29942=CARTESIAN_POINT('',(0.00307739856515751,-0.006584136793575,-0.00799766552221159));
#29943=CARTESIAN_POINT('',(0.00104914963355874,-0.00719080424345263,-0.00792529089947053));
#29944=CARTESIAN_POINT('',(-3.34944636342081E-5,-0.00726739517749434,-0.00788894703453013));
#29945=CARTESIAN_POINT('',(-0.00212526001481185,-0.00694913026412326,-0.00781673225072299));
#29946=CARTESIAN_POINT('',(-0.00313717349682018,-0.00655508924529774,-0.00778029953442967));
#29947=CARTESIAN_POINT('',(-0.0048920509960518,-0.00537377340643036,-0.0077081382353889));
#29948=CARTESIAN_POINT('',(-0.00563810758355737,-0.00458471425111287,-0.00767170574096235));
#29949=CARTESIAN_POINT('',(-0.00672019050133935,-0.00276650849877687,-0.007599490420902));
#29950=CARTESIAN_POINT('',(-0.0070568248862266,-0.0017347138678294,-0.00756314712841486));
#29951=CARTESIAN_POINT('',(-0.00725818469883238,0.00037272372944407,-0.00749077165697859));
#29952=CARTESIAN_POINT('',(-0.00712145809453643,0.00144818120252497,-0.00745460436470009));
#29953=CARTESIAN_POINT('',(-0.00640171583705767,0.00344126714831625,-0.00738196647476595));
#29954=CARTESIAN_POINT('',(-0.00581957893249744,0.00435360342525378,-0.00734605742492407));
#29955=CARTESIAN_POINT('',(-0.00431418952361361,0.00584909992429122,-0.00727306178765397));
#29956=CARTESIAN_POINT('',(-0.00339778106204424,0.00642487332653685,-0.0072371524434806));
#29957=CARTESIAN_POINT('',(-0.00139990793571579,0.00713121855472527,-0.00716451528284037));
#29958=CARTESIAN_POINT('',(-0.000323505480400539,0.0072606186685073,-0.0071283473403949));
#29959=CARTESIAN_POINT('',(0.00178251377636377,0.00704492904565687,-0.00705597271765075));
#29960=CARTESIAN_POINT('',(0.00281205658027764,0.00670137988284672,-0.00701962885271883));
#29961=CARTESIAN_POINT('',(0.00462280125037804,0.00560685742264555,-0.00694741406889786));
#29962=CARTESIAN_POINT('',(0.00540689443550218,0.00485556846583332,-0.00691098135260347));
#29963=CARTESIAN_POINT('',(0.0065761198391736,0.00309261239607762,-0.00683882005357878));
#29964=CARTESIAN_POINT('',(0.00696342638457993,0.00207811329689597,-0.00680238755913261));
#29965=CARTESIAN_POINT('',(0.00726734342673805,-1.57849886626648E-5,-0.00673017223909525));
#29966=CARTESIAN_POINT('',(0.00718350233401858,-0.00109786333181072,-0.00669382894658713));
#29967=CARTESIAN_POINT('',(0.00656305309032466,-0.00312193885820372,-0.00662145347516986));
#29968=CARTESIAN_POINT('',(0.00602517442191273,-0.00406320899944546,-0.00658528618287567));
#29969=CARTESIAN_POINT('',(0.00459749831080146,-0.00562914687378486,-0.00651264829295377));
#29970=CARTESIAN_POINT('',(0.00371053796163789,-0.00624926153807326,-0.00647673924310246));
#29971=CARTESIAN_POINT('',(0.00174743776496527,-0.00705483255843322,-0.00640374360583926));
#29972=CARTESIAN_POINT('',(0.000680447802063739,-0.00723608348461835,-0.00636783426165505));
#29973=CARTESIAN_POINT('',(-0.001435652904262,-0.00712410843840487,-0.00629519710102939));
#29974=CARTESIAN_POINT('',(-0.00247963838116228,-0.00683173716883558,-0.00625902915857182));
#29975=CARTESIAN_POINT('',(-0.00434280562236072,-0.00582652726309626,-0.0061866545358375));
#29976=CARTESIAN_POINT('',(-0.00516250857393213,-0.00511514024919673,-0.00615031067090406));
#29977=CARTESIAN_POINT('',(-0.0064165629013749,-0.00341099136485332,-0.00607809588707619));
#29978=CARTESIAN_POINT('',(-0.00685346470999765,-0.00241683140327485,-0.00604166317078753));
#29979=CARTESIAN_POINT('',(-0.00725903404946125,-0.000340629183025838,-0.00596950187175825));
#29980=CARTESIAN_POINT('',(-0.00722862664216142,0.000744861568631085,-0.00593306937731475));
#29981=CARTESIAN_POINT('',(-0.00670810919405233,0.00279567535466952,-0.00586085405727664));
#29982=CARTESIAN_POINT('',(-0.00621655667006064,0.00376330079133864,-0.00582451076477202));
#29983=CARTESIAN_POINT('',(-0.00486875614304572,0.00539586709624651,-0.00575213529334864));
#29984=CARTESIAN_POINT('',(-0.00401161256188314,0.00605965005927102,-0.00571596800107702));
#29985=CARTESIAN_POINT('',(-0.0020933533431652,0.00696004001606832,-0.00564333011111602));
#29986=CARTESIAN_POINT('',(-0.00103660122222697,0.00719352623141683,-0.00560742106129653));
#29987=CARTESIAN_POINT('',(0.00108534555283438,0.00718653088777161,-0.00553442542400878));
#29988=CARTESIAN_POINT('',(0.00214047746750604,0.00694566552741994,-0.00549851607983565));
#29989=CARTESIAN_POINT('',(0.0040526486037888,0.0060324173925454,-0.0054258789192123));
#29990=CARTESIAN_POINT('',(0.00490527977717149,0.00536278561505491,-0.00538971097675477));
#29991=CARTESIAN_POINT('',(0.00624194467998492,0.00372108952233504,-0.00531733635401815));
#29992=CARTESIAN_POINT('',(0.00672701543546565,0.00275016688147177,-0.00528099248907933));
#29993=CARTESIAN_POINT('',(0.0072334610169168,0.000695832792476032,-0.00520877770526449));
#29994=CARTESIAN_POINT('',(0.0072566571092038,-0.000389846331799926,-0.00517234498897591));
#29995=CARTESIAN_POINT('',(0.00683682612902857,-0.00246321173532627,-0.00510018368993359));
#29996=CARTESIAN_POINT('',(0.00639333402113973,-0.00345443801252004,-0.00506375119549885));
#29997=CARTESIAN_POINT('',(0.00512762614573075,-0.0051499494907857,-0.00499153587545613));
#29998=CARTESIAN_POINT('',(0.00430319660631324,-0.00585580981979079,-0.00495519258295575));
#29999=CARTESIAN_POINT('',(0.00243323520837126,-0.00684832348254423,-0.00488281711152852));
#30000=CARTESIAN_POINT('',(0.00138731905467838,-0.00713356432844633,-0.0048466498192527));
#30001=CARTESIAN_POINT('',(-0.00072948569468554,-0.00723133015881576,-0.00477401192930397));
#30002=CARTESIAN_POINT('',(-0.00179514865645575,-0.00704264176550899,-0.00473810287945765));
#30003=CARTESIAN_POINT('',(-0.00375289484889557,-0.00622414503550719,-0.00466510724221132));
#30004=CARTESIAN_POINT('',(-0.00463553444612406,-0.00559783295628993,-0.00462919789801713));
#30005=CARTESIAN_POINT('',(-0.00605266529073802,-0.00402234548266793,-0.00455656073739454));
#30006=CARTESIAN_POINT('',(-0.00658413679357753,-0.00307739856515646,-0.00452039279493507));
#30007=CARTESIAN_POINT('',(-0.00719080424345081,-0.00104914963355747,-0.00444801817220151));
#30008=CARTESIAN_POINT('',(-0.00726739517749341,3.34944636354764E-5,-0.00441167430725886));
#30009=CARTESIAN_POINT('',(-0.00694913026412382,0.00212526001481356,-0.00433945952344863));
#30010=CARTESIAN_POINT('',(-0.00655508924530171,0.00313717349682264,-0.00430302680714884));
#30011=CARTESIAN_POINT('',(-0.00537377340642612,0.00489205099604989,-0.00423086550812416));
#30012=CARTESIAN_POINT('',(-0.00458471425111404,0.00563810758356184,-0.00419443301368414));
#30013=CARTESIAN_POINT('',(-0.00276650849877146,0.00672019050133746,-0.00412221769363452));
#30014=CARTESIAN_POINT('',(-0.00173471386783098,0.00705682488623278,-0.00408587440113144));
#30015=CARTESIAN_POINT('',(0.000372723729446471,0.00725818469882635,-0.0040134989297165));
#30016=CARTESIAN_POINT('',(0.00144818120252681,0.00712145809453751,-0.00397733163742573));
#30017=CARTESIAN_POINT('',(0.00344126714831952,0.00640171583705481,-0.00390469374749465));
#30018=CARTESIAN_POINT('',(0.00435360342525374,0.00581957893249987,-0.00386878469764982));
#30019=CARTESIAN_POINT('',(0.00584909992429147,0.00431418952361097,-0.00379578906038278));
#30020=CARTESIAN_POINT('',(0.00642487332654076,0.00339778106204067,-0.00375987971620468));
#30021=CARTESIAN_POINT('',(0.00713121855472419,0.00139990793571129,-0.00368724255557058));
#30022=CARTESIAN_POINT('',(0.00726061866851071,0.000323505480401402,-0.00365107461311612));
#30023=CARTESIAN_POINT('',(0.00704492904565339,-0.00178251377636519,-0.0035786999903841));
#30024=CARTESIAN_POINT('',(0.00670137988284643,-0.00281205658028245,-0.00354235612544367));
#30025=CARTESIAN_POINT('',(0.00560685742264143,-0.00462280125038053,-0.00347014134162729));
#30026=CARTESIAN_POINT('',(0.00485556846582585,-0.00540689443550281,-0.00343370862533945));
#30027=CARTESIAN_POINT('',(0.0030926123960786,-0.00657611983917729,-0.00336154732629711));
#30028=CARTESIAN_POINT('',(0.00207811329689281,-0.00696342638458015,-0.00332511483186319));
#30029=CARTESIAN_POINT('',(-1.57849886678835E-5,-0.00726734342673904,-0.00325289951181893));
#30030=CARTESIAN_POINT('',(-0.00109786333180993,-0.00718350233401927,-0.00321655621931441));
#30031=CARTESIAN_POINT('',(-0.0031219388582049,-0.00656305309032384,-0.00314418074789715));
#30032=CARTESIAN_POINT('',(-0.00406320899944794,-0.00602517442190716,-0.00310801345561085));
#30033=CARTESIAN_POINT('',(-0.00562914687378846,-0.00459749831080149,-0.00303537556567285));
#30034=CARTESIAN_POINT('',(-0.00624926153807508,-0.0037105379616394,-0.0029994665158259));
#30035=CARTESIAN_POINT('',(-0.00705483255843151,-0.0017474377649635,-0.00292647087857037));
#30036=CARTESIAN_POINT('',(-0.00723608348461909,-0.000680447802060205,-0.00289056153438103));
#30037=CARTESIAN_POINT('',(-0.0071241084384037,0.0014356529042668,-0.00281792437375769));
#30038=CARTESIAN_POINT('',(-0.00683173716883591,0.00247963838116247,-0.00278175643129986));
#30039=CARTESIAN_POINT('',(-0.00582652726309597,0.00434280562236042,-0.00270938180856403));
#30040=CARTESIAN_POINT('',(-0.00511514024919768,0.00516250857393693,-0.00267303794362471));
#30041=CARTESIAN_POINT('',(-0.0034109913648488,0.00641656290137277,-0.00260082315980989));
#30042=CARTESIAN_POINT('',(-0.00241683140327436,0.00685346470999906,-0.00256439044351557));
#30043=CARTESIAN_POINT('',(-0.000340629183025886,0.00725903404945992,-0.00249222914448476));
#30044=CARTESIAN_POINT('',(0.000744861568633197,0.00722862664216346,-0.00245579665004158));
#30045=CARTESIAN_POINT('',(0.00279567535467062,0.00670810919404948,-0.00238358133000424));
#30046=CARTESIAN_POINT('',(0.00376330079133947,0.00621655667006173,-0.0023472380374981));
#30047=CARTESIAN_POINT('',(0.00539586709624765,0.00486875614304302,-0.00227486256607702));
#30048=CARTESIAN_POINT('',(0.00605965005927792,0.0040116125618877,-0.00223869527378932));
#30049=CARTESIAN_POINT('',(0.00696004001606203,0.00209335334315932,-0.00216605738385825));
#30050=CARTESIAN_POINT('',(0.00719352623141566,0.00103660122222664,-0.00213014833401346));
#30051=CARTESIAN_POINT('',(0.00718653088777276,-0.00108534555283466,-0.00205715269674642));
#30052=CARTESIAN_POINT('',(0.00694566552742021,-0.00214047746750529,-0.00202124335256258));
#30053=CARTESIAN_POINT('',(0.0060324173925453,-0.00405264860378919,-0.00194860619194));
#30054=CARTESIAN_POINT('',(0.00536278561505485,-0.00490527977717104,-0.00191243824948167));
#30055=CARTESIAN_POINT('',(0.0037210895223348,-0.00624194467998561,-0.00184006362674582));
#30056=CARTESIAN_POINT('',(0.00275016688147183,-0.0067270154354661,-0.00180371976180508));
#30057=CARTESIAN_POINT('',(0.000695832792475538,-0.00723346101691648,-0.00173150497799332));
#30058=CARTESIAN_POINT('',(-0.000389846331799945,-0.00725665710920745,-0.00169507226169586));
#30059=CARTESIAN_POINT('',(-0.00246321173532793,-0.00683682612902454,-0.00162291096266811));
#30060=CARTESIAN_POINT('',(-0.0034544380125203,-0.00639333402113907,-0.00158647846822539));
#30061=CARTESIAN_POINT('',(-0.0051499494907848,-0.00512762614573182,-0.00151426314818421));
#30062=CARTESIAN_POINT('',(-0.00585580981979337,-0.00430319660631435,-0.00147791985567843));
#30063=CARTESIAN_POINT('',(-0.00684832348254183,-0.0024332352083697,-0.00140554438426041));
#30064=CARTESIAN_POINT('',(-0.00713356432844919,-0.00138731905467894,-0.00136937709197385));
#30065=CARTESIAN_POINT('',(-0.00723133015881286,0.000729485694686566,-0.0012967392020374));
#30066=CARTESIAN_POINT('',(-0.00704264176550485,0.00179514865645567,-0.00126083015219145));
#30067=CARTESIAN_POINT('',(-0.0062241450355111,0.00375289484889606,-0.00118783451493208));
#30068=CARTESIAN_POINT('',(-0.00559783295628811,0.00463553444612332,-0.0011519251707444));
#30069=CARTESIAN_POINT('',(-0.00402234548266938,0.00605266529073901,-0.00107928801012182));
#30070=CARTESIAN_POINT('',(-0.00307739856515607,0.00658413679357564,-0.00104312006766541));
#30071=CARTESIAN_POINT('',(-0.00104914963355747,0.00719080424345277,-0.000970745444925725));
#30072=CARTESIAN_POINT('',(3.34944636362563E-5,0.00726739517749143,-0.000934401579989581));
#30073=CARTESIAN_POINT('',(0.00212526001481323,0.00694913026412567,-0.00086218679617245));
#30074=CARTESIAN_POINT('',(0.00313717349682277,0.00655508924530081,-0.000825754079879204));
#30075=CARTESIAN_POINT('',(0.00489205099605003,0.00537377340642675,-0.000753592780848384));
#30076=CARTESIAN_POINT('',(0.0056381075835625,0.00458471425111558,-0.000717160286406051));
#30077=CARTESIAN_POINT('',(0.00672019050133696,0.00276650849876955,-0.00064494496636717));
#30078=CARTESIAN_POINT('',(0.00705682488623223,0.00173471386782946,-0.000608601673859866));
#30079=CARTESIAN_POINT('',(0.00725818469882695,-0.000372723729446043,-0.000536226202442616));
#30080=CARTESIAN_POINT('',(0.00712145809453642,-0.00144818120252827,-0.000500058910156047));
#30081=CARTESIAN_POINT('',(0.00640171583705524,-0.00344126714831973,-0.000427421020218825));
#30082=CARTESIAN_POINT('',(0.00581957893250037,-0.00435360342525503,-0.000391511970372879));
#30083=CARTESIAN_POINT('',(0.00431418952361021,-0.00584909992429036,-0.000318516333114281));
#30084=CARTESIAN_POINT('',(0.00339778106204239,-0.00642487332654475,-0.000282606988926975));
#30085=CARTESIAN_POINT('',(0.00139990793570993,-0.00713121855472002,-0.00020996982830286));
#30086=CARTESIAN_POINT('',(0.000323505480399655,-0.00726061866851029,-0.000173801885847229));
#30087=CARTESIAN_POINT('',(-0.0017825137763636,-0.00704492904565378,-0.000101427263107548));
#30088=CARTESIAN_POINT('',(-0.00281205658028296,-0.00670137988284679,-6.50833981679304E-5));
#30089=CARTESIAN_POINT('',(-0.0046228012503775,-0.00560685742264234,7.13138564229714E-6));
#30090=CARTESIAN_POINT('',(-0.00540689443550383,-0.00485556846583195,4.3564101940445E-5));
#30091=CARTESIAN_POINT('',(-0.00657611983917429,-0.00309261239607615,0.000115725400968197));
#30092=CARTESIAN_POINT('',(-0.00696342638458038,-0.00207811329689332,0.000152157895411852));
#30093=CARTESIAN_POINT('',(-0.00726734342673808,1.57849886669528E-5,0.0002243732154515));
#30094=CARTESIAN_POINT('',(-0.00718350233401693,0.00109786333180495,0.000260716507958075));
#30095=CARTESIAN_POINT('',(-0.00656305309032657,0.00312193885819541,0.000333091979374559));
#30096=CARTESIAN_POINT('',(-0.00602517442193104,0.00406320899947221,0.000369259271663406));
#30097=CARTESIAN_POINT('',(-0.00459749831074794,0.00562914687383506,0.000441897161614154));
#30098=CARTESIAN_POINT('',(-0.00371053796151535,0.00624926153783101,0.000477806211348708));
#30099=CARTESIAN_POINT('',(-0.00174743776551818,0.00705483255842964,0.000550801848655444));
#30100=CARTESIAN_POINT('',(-0.000680447801294133,0.00723608348588212,0.000586711193786415));
#30101=CARTESIAN_POINT('',(0.00143565290608666,0.0071241084365796,0.000659348353022638));
#30102=CARTESIAN_POINT('',(0.00247963837529481,0.00683173716790875,0.000695516292370224));
#30103=CARTESIAN_POINT('',(0.0043428056206459,0.00582652727327286,0.00076789092290518));
#30104=CARTESIAN_POINT('',(0.00516250859039049,0.00511514023630632,0.000804234794196687));
#30105=CARTESIAN_POINT('',(0.00641656289023011,0.00341099133157275,0.0008764495419424));
#30106=CARTESIAN_POINT('',(0.00685346469520728,0.00241683146463233,0.000912882267660161));
#30107=CARTESIAN_POINT('',(0.00725903411303602,0.000340629271551516,0.00098504370920131));
#30108=CARTESIAN_POINT('',(0.00722862665697431,-0.000744861703369959,0.00102147602741882));
#30109=CARTESIAN_POINT('',(0.00670810890042664,-0.00279567567614128,0.00109369086559387));
#30110=CARTESIAN_POINT('',(0.00621655607651332,-0.00376330035189889,0.00113003525147544));
#30111=CARTESIAN_POINT('',(0.00486875838265234,-0.00539586578431444,0.00120241207477105));
#30112=CARTESIAN_POINT('',(0.00401161662392975,-0.00605965436823582,0.00123857449452884));
#30113=CARTESIAN_POINT('',(0.00209333657742418,-0.00696004077825442,0.0013112095800839));
#30114=CARTESIAN_POINT('',(0.00103659171941237,-0.00719350430124366,0.00134715113465353));
#30115=CARTESIAN_POINT('',(-0.00191041971977791,-0.00718386892224559,0.00144849411294274));
#30116=CARTESIAN_POINT('',(-0.00377227819610396,-0.00640401708981634,0.00151212929633834));
#30117=CARTESIAN_POINT('',(-0.0064299244082464,-0.00373033709005478,0.00164156781191397));
#30118=CARTESIAN_POINT('',(-0.00719625087246649,-0.00185395380901434,0.00170544297515432));
#30119=CARTESIAN_POINT('',(-0.00719005711644639,2.43665513196906E-5,0.00177004279007146));
#30120=CARTESIAN_POINT('',(-0.00719,-2.43712308654023E-5,-0.0140410700265819));
#30121=CARTESIAN_POINT('',(-0.00719309747276633,0.000914781327291283,-0.0140087701339982));
#30122=CARTESIAN_POINT('',(-0.00701046692282683,0.00185383013393277,-0.0139769826252248));
#30123=CARTESIAN_POINT('',(-0.00584628899116327,0.00469565481227827,-0.0138710392878109));
#30124=CARTESIAN_POINT('',(-0.00413420496023883,0.00625264525909713,-0.0137993589218868));
#30125=CARTESIAN_POINT('',(-0.00109778115756082,0.00718353970545525,-0.0136908149277581));
#30126=CARTESIAN_POINT('',(-1.57621275787881E-5,0.00726727668491749,-0.013654505956057));
#30127=CARTESIAN_POINT('',(0.0020780670851226,0.00696336385150681,-0.0135822796027047));
#30128=CARTESIAN_POINT('',(0.00309258005265746,0.00657607392611431,-0.0135458386651108));
#30129=CARTESIAN_POINT('',(0.00485553091203102,0.00540685351702608,-0.0134736824086932));
#30130=CARTESIAN_POINT('',(0.00560681015793595,0.00462276743850325,-0.0134372508723692));
#30131=CARTESIAN_POINT('',(0.00670132423911886,0.00281203924609828,-0.0133650342858113));
#30132=CARTESIAN_POINT('',(0.00704487175681332,0.0017825046314887,-0.0133286905839261));
#30133=CARTESIAN_POINT('',(0.00726056134134748,-0.000323498100568699,-0.0132563164906695));
#30134=CARTESIAN_POINT('',(0.00713116287663823,-0.00139989213428312,-0.013220148364931));
#30135=CARTESIAN_POINT('',(0.00642482455556629,-0.00339774967419534,-0.0131475110777197));
#30136=CARTESIAN_POINT('',(0.00584905635718351,-0.00431415134828831,-0.0131116018059614));
#30137=CARTESIAN_POINT('',(0.00435357284755307,-0.00581952969982387,-0.0130386062056008));
#30138=CARTESIAN_POINT('',(0.00344124413936916,-0.00640166266807087,-0.0130026971236706));
#30139=CARTESIAN_POINT('',(0.00144817457480563,-0.00712140051957246,-0.0129300592451617));
#30140=CARTESIAN_POINT('',(0.000372725724967005,-0.00725812679414896,-0.0128938919514255));
#30141=CARTESIAN_POINT('',(-0.00173469529522488,-0.00705677001193887,-0.012821516476213));
#30142=CARTESIAN_POINT('',(-0.00276648191979289,-0.00672013901723145,-0.0127851731895264));
#30143=CARTESIAN_POINT('',(-0.00458467403739847,-0.00563806590143227,-0.012712957858533));
#30144=CARTESIAN_POINT('',(-0.00537372737395455,-0.00489201581532433,-0.0126765253742606));
#30145=CARTESIAN_POINT('',(-0.00655503508825474,-0.00313715298829169,-0.0126043640616781));
#30146=CARTESIAN_POINT('',(-0.00694907362059592,-0.00212524786670271,-0.0125679313555053));
#30147=CARTESIAN_POINT('',(-0.00726733745110847,-3.34990726667784E-5,-0.012495716560779));
#30148=CARTESIAN_POINT('',(-0.0071907478402206,0.0010491364390741,-0.0124593727016529));
#30149=CARTESIAN_POINT('',(-0.00658408658164294,0.00307736969557237,-0.0123869980757161));
#30150=CARTESIAN_POINT('',(-0.00605261991751576,0.00402230947970013,-0.0123508301306084));
#30151=CARTESIAN_POINT('',(-0.00463550142938601,0.00559778534343702,-0.0122781929793886));
#30152=CARTESIAN_POINT('',(-0.00375286918367178,0.00622409311106949,-0.0122422836201452));
#30153=CARTESIAN_POINT('',(-0.00179513925007463,0.00704258456041726,-0.0121692880094645));
#30154=CARTESIAN_POINT('',(-0.000729484790171836,0.00723127223232546,-0.0121333789446197));
#30155=CARTESIAN_POINT('',(0.00138730314760839,0.00713350860255954,-0.0120607410639456));
#30156=CARTESIAN_POINT('',(0.00243321120648015,0.00684827074844557,-0.0120245737691142));
#30157=CARTESIAN_POINT('',(0.00430315844720215,0.00585576622976275,-0.0119521982943733));
#30158=CARTESIAN_POINT('',(0.00512758188781125,0.00514991209723695,-0.0119158550077828));
#30159=CARTESIAN_POINT('',(0.00639328091757387,0.00345441489233318,-0.0118436396767009));
#30160=CARTESIAN_POINT('',(0.00683677013747896,0.0024631968483955,-0.0118072071924502));
#30161=CARTESIAN_POINT('',(0.00725659922633007,0.000389848109405319,-0.011735045879847));
#30162=CARTESIAN_POINT('',(0.00723340403624636,-0.000695822339324392,-0.0116986131736994));
#30163=CARTESIAN_POINT('',(0.00672696386703592,-0.00275014053235113,-0.0116263983789488));
#30164=CARTESIAN_POINT('',(0.00624189761949387,-0.00372105574763302,-0.0115900545198076));
#30165=CARTESIAN_POINT('',(0.00490524443531421,-0.00536273972777125,-0.0115176798939249));
#30166=CARTESIAN_POINT('',(0.00405262046213646,-0.00603236676656215,-0.0114815119487978));
#30167=CARTESIAN_POINT('',(0.00214046518466179,-0.00694560890392152,-0.0114088747975626));
#30168=CARTESIAN_POINT('',(0.00108534171188601,-0.00718647309418859,-0.0113729654383349));
#30169=CARTESIAN_POINT('',(-0.00103658802115338,-0.00719346978113902,-0.0112999698276385));
#30170=CARTESIAN_POINT('',(-0.00209333201131658,-0.0069599861528186,-0.0112640607627929));
#30171=CARTESIAN_POINT('',(-0.00401157654030057,-0.00605960466264294,-0.0111914228821357));
#30172=CARTESIAN_POINT('',(-0.00486871378773508,-0.00539582756142553,-0.0111552555873162));
#30173=CARTESIAN_POINT('',(-0.00621650473444587,-0.0037632751222566,-0.011082880112535));
#30174=CARTESIAN_POINT('',(-0.00670805399516715,-0.00279565774430619,-0.0110465368259488));
#30175=CARTESIAN_POINT('',(-0.00722856873315945,-0.000744860530218091,-0.0109743214948983));
#30176=CARTESIAN_POINT('',(-0.00725897662301592,0.000340621509716384,-0.0109378890105921));
#30177=CARTESIAN_POINT('',(-0.00685341191347264,0.00241680761016474,-0.0108657276980687));
#30178=CARTESIAN_POINT('',(-0.00641651425833895,0.00341095990183559,-0.0108292949918682));
#30179=CARTESIAN_POINT('',(-0.00516247101429667,0.00511509617140522,-0.0107570801971437));
#30180=CARTESIAN_POINT('',(-0.00434277506916309,0.00582647805008706,-0.0107207363380231));
#30181=CARTESIAN_POINT('',(-0.00247962328983785,0.00683168124975376,-0.0106483617120729));
#30182=CARTESIAN_POINT('',(-0.00143564627849434,0.0071240508967529,-0.0106121937669828));
#30183=CARTESIAN_POINT('',(0.000680437481053837,0.00723602647088379,-0.0105395566157415));
#30184=CARTESIAN_POINT('',(0.00174741919689521,0.00705477769426572,-0.0105036472565332));
#30185=CARTESIAN_POINT('',(0.00371050416284737,0.00624921443664078,-0.0104306516458038));
#30186=CARTESIAN_POINT('',(0.00459745799018133,0.00562910527398703,-0.0103947425809817));
#30187=CARTESIAN_POINT('',(0.0060251237697562,0.00406318084328688,-0.0103221047003107));
#30188=CARTESIAN_POINT('',(0.00656299882979235,0.00312191854146624,-0.0102859374054834));
#30189=CARTESIAN_POINT('',(0.00718344452864146,0.00109785949157134,-0.0102135619307314));
#30190=CARTESIAN_POINT('',(0.00726728569041279,1.57898425179862E-5,-0.0101772186441096));
#30191=CARTESIAN_POINT('',(0.00696337248626668,-0.0020780920954515,-0.0101050033131013));
#30192=CARTESIAN_POINT('',(0.00657606972051115,-0.00309258333071337,-0.0100685708287816));
#30193=CARTESIAN_POINT('',(0.00540685476309802,-0.00485552627950851,-0.00999640951624288));
#30194=CARTESIAN_POINT('',(0.00462276835045015,-0.00560680973971266,-0.00995997681002896));
#30195=CARTESIAN_POINT('',(0.00281203874754511,-0.00670132478683354,-0.0098877620153467));
#30196=CARTESIAN_POINT('',(0.00178250438189289,-0.00704487188654584,-0.00985141815618041));
#30197=CARTESIAN_POINT('',(-0.000323498023658633,-0.0072605612308287,-0.0097790435302793));
#30198=CARTESIAN_POINT('',(-0.00139989203688523,-0.00713116285759408,-0.00974287558516111));
#30199=CARTESIAN_POINT('',(-0.00339774970846165,-0.00642482460240109,-0.00967023843392671));
#30200=CARTESIAN_POINT('',(-0.00431415137335821,-0.00584905634211228,-0.00963432907474912));
#30201=CARTESIAN_POINT('',(-0.00581952968153659,-0.00435357284343158,-0.0095613334639515));
#30202=CARTESIAN_POINT('',(-0.00640166266610289,-0.00344124414514989,-0.00952542439916768));
#30203=CARTESIAN_POINT('',(-0.00712140052315398,-0.00144817457337093,-0.00945278651848825));
#30204=CARTESIAN_POINT('',(-0.00725812679376296,-0.000372725723830902,-0.00941661922368434));
#30205=CARTESIAN_POINT('',(-0.00705677001142131,0.00173469529458462,-0.00934424374889396));
#30206=CARTESIAN_POINT('',(-0.00672013901740774,0.0027664819196555,-0.00930790046227081));
#30207=CARTESIAN_POINT('',(-0.00563806590146389,0.00458467403754789,-0.00923568513130384));
#30208=CARTESIAN_POINT('',(-0.00489201581527204,0.00537372737394528,-0.00919925264695077));
#30209=CARTESIAN_POINT('',(-0.00313715298830901,0.00655503508825429,-0.00912709133443729));
#30210=CARTESIAN_POINT('',(-0.0021252478667098,0.00694907362059298,-0.00909065862822848));
#30211=CARTESIAN_POINT('',(-3.34990726673003E-5,0.00726733745111181,-0.00901844383351088));
#30212=CARTESIAN_POINT('',(0.0010491364390763,0.00719074784022145,-0.00898209997438099));
#30213=CARTESIAN_POINT('',(0.00307736969557334,0.00658408658164155,-0.00890972534844229));
#30214=CARTESIAN_POINT('',(0.00402230947970229,0.00605261991751987,-0.00887355740334446));
#30215=CARTESIAN_POINT('',(0.00559778534343459,0.00463550142938187,-0.008800920252107));
#30216=CARTESIAN_POINT('',(0.00622409311107522,0.00375286918367609,-0.00876501089289031));
#30217=CARTESIAN_POINT('',(0.0070425845604117,0.00179513925006985,-0.00869201528217398));
#30218=CARTESIAN_POINT('',(0.00723127223231931,0.000729484790173338,-0.00865610621733461));
#30219=CARTESIAN_POINT('',(0.00713350860256567,-0.00138730314760929,-0.0085834683366851));
#30220=CARTESIAN_POINT('',(0.0068482707484462,-0.00243321120648243,-0.00854730104184166));
#30221=CARTESIAN_POINT('',(0.00585576622976196,-0.00430315844720011,-0.00847492556710038));
#30222=CARTESIAN_POINT('',(0.00514991209723149,-0.00512758188779838,-0.00843858228048562));
#30223=CARTESIAN_POINT('',(0.00345441489234066,-0.00639328091758518,-0.0083663669494527));
#30224=CARTESIAN_POINT('',(0.00246319684839438,-0.00683677013746513,-0.00832993446515067));
#30225=CARTESIAN_POINT('',(0.000389848109409576,-0.00725659922634325,-0.00825777315260114));
#30226=CARTESIAN_POINT('',(-0.000695822339321421,-0.00723340403624211,-0.00822134044641911));
#30227=CARTESIAN_POINT('',(-0.00275014053234976,-0.00672696386704125,-0.00814912565168388));
#30228=CARTESIAN_POINT('',(-0.00372105574763575,-0.00624189761949856,-0.00811278179254448));
#30229=CARTESIAN_POINT('',(-0.00536273972776876,-0.00490524443530932,-0.00804040716664259));
#30230=CARTESIAN_POINT('',(-0.00603236676656028,-0.00405262046213817,-0.00800423922152594));
#30231=CARTESIAN_POINT('',(-0.00694560890392066,-0.00214046518466569,-0.00793160207028925));
#30232=CARTESIAN_POINT('',(-0.00718647309418995,-0.00108534171188497,-0.00789569271106792));
#30233=CARTESIAN_POINT('',(-0.00719346978113769,0.00103658802115313,-0.00782269710036002));
#30234=CARTESIAN_POINT('',(-0.00695998615282404,0.00209333201131557,-0.00778678803553218));
#30235=CARTESIAN_POINT('',(-0.00605960466264018,0.00401157654029584,-0.00771415015485122));
#30236=CARTESIAN_POINT('',(-0.00539582756142664,0.00486871378774006,-0.00767798286005378));
#30237=CARTESIAN_POINT('',(-0.00376327512225495,0.00621650473444129,-0.0076056073852519));
#30238=CARTESIAN_POINT('',(-0.00279565774430927,0.00670805399516752,-0.00756926409868168));
#30239=CARTESIAN_POINT('',(-0.000744860530220048,0.00722856873315786,-0.00749704876762038));
#30240=CARTESIAN_POINT('',(0.000340621509718325,0.00725897662302272,-0.00746061628333479));
#30241=CARTESIAN_POINT('',(0.00241680761016268,0.00685341191346589,-0.00738845497078066));
#30242=CARTESIAN_POINT('',(0.00341095990183554,0.0064165142583411,-0.00735202226459938));
#30243=CARTESIAN_POINT('',(0.00511509617140321,0.00516247101429606,-0.0072798074698672));
#30244=CARTESIAN_POINT('',(0.00582647805007756,0.0043427750691594,-0.00724346361073014));
#30245=CARTESIAN_POINT('',(0.00683168124976245,0.00247962328984308,-0.00717108898482058));
#30246=CARTESIAN_POINT('',(0.00712405089675078,0.00143564627849451,-0.00713492103970666));
#30247=CARTESIAN_POINT('',(0.0072360264708859,-0.000680437481053441,-0.00706228388847226));
#30248=CARTESIAN_POINT('',(0.00705477769426897,-0.00174741919689787,-0.00702637452926781));
#30249=CARTESIAN_POINT('',(0.00624921443663749,-0.00371050416284487,-0.00695337891852387));
#30250=CARTESIAN_POINT('',(0.00562910527398633,-0.00459745799018292,-0.00691746985371441));
#30251=CARTESIAN_POINT('',(0.00406318084328793,-0.00602512376975431,-0.00684483197303269));
#30252=CARTESIAN_POINT('',(0.00312191854146655,-0.00656299882979698,-0.00680866467822031));
#30253=CARTESIAN_POINT('',(0.00109785949157234,-0.00718344452863644,-0.00673628920344911));
#30254=CARTESIAN_POINT('',(1.57898425157631E-5,-0.0072672856904205,-0.00669994591685016));
#30255=CARTESIAN_POINT('',(-0.00207809209544696,-0.00696337248625942,-0.0066277305858157));
#30256=CARTESIAN_POINT('',(-0.00309258333072013,-0.00657606972051688,-0.00659129810152624));
#30257=CARTESIAN_POINT('',(-0.00485552627950234,-0.00540685476309198,-0.00651913678895295));
#30258=CARTESIAN_POINT('',(-0.00560680973972307,-0.00462276835045597,-0.00648270408278328));
#30259=CARTESIAN_POINT('',(-0.00670132478682111,-0.00281203874754279,-0.00641048928804727));
#30260=CARTESIAN_POINT('',(-0.00704487188655621,-0.0017825043818928,-0.00637414542892963));
#30261=CARTESIAN_POINT('',(-0.00726056123081833,0.00032349802365789,-0.00630177080298481));
#30262=CARTESIAN_POINT('',(-0.00713116285758991,0.0013998920368823,-0.00626560285788283));
#30263=CARTESIAN_POINT('',(-0.00642482460240738,0.00339774970845881,-0.00619296570665995));
#30264=CARTESIAN_POINT('',(-0.00584905634210328,0.00431415137334864,-0.00615705634745419));
#30265=CARTESIAN_POINT('',(-0.00435357284344004,0.00581952968154678,-0.00608406073670106));
#30266=CARTESIAN_POINT('',(-0.00344124414515375,0.00640166266610718,-0.00604815167190321));
#30267=CARTESIAN_POINT('',(-0.00144817457337304,0.00712140052314761,-0.00597551379120768));
#30268=CARTESIAN_POINT('',(-0.000372725723831925,0.00725812679375837,-0.00593934649640361));
#30269=CARTESIAN_POINT('',(0.00173469529458617,0.0070567700114259,-0.00586697102162934));
#30270=CARTESIAN_POINT('',(0.00276648191966689,0.0067201390174245,-0.00583062773503884));
#30271=CARTESIAN_POINT('',(0.00458467403753271,0.0056380659014494,-0.00575841240399055));
#30272=CARTESIAN_POINT('',(0.00537372737395314,0.00489201581527671,-0.00572197991969736));
#30273=CARTESIAN_POINT('',(0.00655503508824469,0.00313715298830708,-0.00564981860714551));
#30274=CARTESIAN_POINT('',(0.00694907362059124,0.00212524786670918,-0.00561338590095199));
#30275=CARTESIAN_POINT('',(0.00726733745111319,3.34990726703471E-5,-0.00554117110624206));
#30276=CARTESIAN_POINT('',(0.00719074784021865,-0.00104913643907644,-0.00550482724710189));
#30277=CARTESIAN_POINT('',(0.00658408658164423,-0.00307736969557393,-0.00543245262117609));
#30278=CARTESIAN_POINT('',(0.00605261991751471,-0.00402230947969808,-0.00539628467605725));
#30279=CARTESIAN_POINT('',(0.00463550142938722,-0.00559778534343868,-0.00532364752484892));
#30280=CARTESIAN_POINT('',(0.00375286918367852,-0.00622409311108351,-0.00528773816563143));
#30281=CARTESIAN_POINT('',(0.00179513925006713,-0.00704258456040356,-0.00521474255488749));
#30282=CARTESIAN_POINT('',(0.000729484790170839,-0.0072312722323272,-0.00517883349007728));
#30283=CARTESIAN_POINT('',(-0.00138730314760581,-0.00713350860255783,-0.00510619560939708));
#30284=CARTESIAN_POINT('',(-0.00243321120648513,-0.00684827074845075,-0.00507002831457975));
#30285=CARTESIAN_POINT('',(-0.00430315844719737,-0.00585576622975746,-0.00499765283981685));
#30286=CARTESIAN_POINT('',(-0.00512758188780396,-0.00514991209723392,-0.00496130955322521));
#30287=CARTESIAN_POINT('',(-0.00639328091758023,-0.0034544148923375,-0.00488909422216774));
#30288=CARTESIAN_POINT('',(-0.00683677013746633,-0.00246319684839675,-0.00485266173788293));
#30289=CARTESIAN_POINT('',(-0.00725659922634214,-0.000389848109406802,-0.00478050042532344));
#30290=CARTESIAN_POINT('',(-0.00723340403623665,0.000695822339320062,-0.00474406771913376));
#30291=CARTESIAN_POINT('',(-0.00672696386704651,0.00275014053235206,-0.00467185292442382));
#30292=CARTESIAN_POINT('',(-0.00624189761950296,0.00372105574764178,-0.0046355090652864));
#30293=CARTESIAN_POINT('',(-0.00490524443530459,0.00536273972776314,-0.00456313443935523));
#30294=CARTESIAN_POINT('',(-0.00405262046213943,0.00603236676656415,-0.00452696649425976));
#30295=CARTESIAN_POINT('',(-0.00214046518466428,0.00694560890391687,-0.00445432934301002));
#30296=CARTESIAN_POINT('',(-0.00108534171188336,0.00718647309421125,-0.0044184199838209));
#30297=CARTESIAN_POINT('',(0.001036588021152,0.00719346978111642,-0.00434542437306162));
#30298=CARTESIAN_POINT('',(0.00209333201131713,0.0069599861528244,-0.00430951530825866));
#30299=CARTESIAN_POINT('',(0.00401157654029508,0.0060596046626394,-0.00423687742757923));
#30300=CARTESIAN_POINT('',(0.00486871378773325,0.00539582756142202,-0.00420071013276347));
#30301=CARTESIAN_POINT('',(0.00621650473444845,0.00376327512225915,-0.00412833465799674));
#30302=CARTESIAN_POINT('',(0.00670805399516244,0.00279565774430914,-0.00409199137139973));
#30303=CARTESIAN_POINT('',(0.00722856873316311,0.000744860530219342,-0.00401977604035683));
#30304=CARTESIAN_POINT('',(0.00725897662302856,-0.000340621509718141,-0.00398334355607171));
#30305=CARTESIAN_POINT('',(0.00685341191346022,-0.00241680761016203,-0.00391118224349841));
#30306=CARTESIAN_POINT('',(0.00641651425833855,-0.00341095990183179,-0.00387474953731824));
#30307=CARTESIAN_POINT('',(0.00516247101429811,-0.0051150961714077,-0.00380253474260294));
#30308=CARTESIAN_POINT('',(0.00434277506916177,-0.00582647805008344,-0.00376619088347242));
#30309=CARTESIAN_POINT('',(0.00247962328983992,-0.00683168124975697,-0.00369381625753282));
#30310=CARTESIAN_POINT('',(0.00143564627849509,-0.00712405089675115,-0.00365764831243543));
#30311=CARTESIAN_POINT('',(-0.000680437481054029,-0.00723602647088551,-0.00358501116119796));
#30312=CARTESIAN_POINT('',(-0.00174741919689655,-0.00705477769426506,-0.00354910180198778));
#30313=CARTESIAN_POINT('',(-0.00371050416284675,-0.0062492144366412,-0.00347610619125841));
#30314=CARTESIAN_POINT('',(-0.00459745799018052,-0.00562910527398658,-0.00344019712643935));
#30315=CARTESIAN_POINT('',(-0.00602512376975749,-0.00406318084328682,-0.00336755924576223));
#30316=CARTESIAN_POINT('',(-0.0065629988297959,-0.00312191854146521,-0.00333139195094262));
#30317=CARTESIAN_POINT('',(-0.00718344452863822,-0.00109785949157136,-0.00325901647618125));
#30318=CARTESIAN_POINT('',(-0.00726728569042009,-1.57898425149358E-5,-0.00322267318957925));
#30319=CARTESIAN_POINT('',(-0.00696337248625936,0.00207809209544908,-0.00315045785854095));
#30320=CARTESIAN_POINT('',(-0.00657606972051391,0.00309258333071823,-0.00311402537424463));
#30321=CARTESIAN_POINT('',(-0.0054068547630946,0.00485552627950473,-0.00304186406168898));
#30322=CARTESIAN_POINT('',(-0.00462276835045416,0.00560680973972331,-0.00300543135550392));
#30323=CARTESIAN_POINT('',(-0.00281203874754034,0.00670132478682342,-0.00293321656078095));
#30324=CARTESIAN_POINT('',(-0.00178250438189282,0.00704487188655298,-0.00289687270164736));
#30325=CARTESIAN_POINT('',(0.000323498023658744,0.00726056123082163,-0.00282449807572156));
#30326=CARTESIAN_POINT('',(0.00139989203688323,0.00713116285759021,-0.00278833013060885));
#30327=CARTESIAN_POINT('',(0.00339774970846299,0.00642482460240528,-0.00271569297938826));
#30328=CARTESIAN_POINT('',(0.00431415137334793,0.00584905634210323,-0.00267978362017918));
#30329=CARTESIAN_POINT('',(0.00581952968154769,0.00435357284343988,-0.00260678800943063));
#30330=CARTESIAN_POINT('',(0.00640166266610557,0.00344124414514944,-0.00257087894462805));
#30331=CARTESIAN_POINT('',(0.00712140052315214,0.00144817457336933,-0.00249824106393712));
#30332=CARTESIAN_POINT('',(0.0072581267937555,0.000372725723834419,-0.00246207376912482));
#30333=CARTESIAN_POINT('',(0.00705677001142875,-0.00173469529458923,-0.00238969829436268));
#30334=CARTESIAN_POINT('',(0.00672013901742156,-0.00276648191966884,-0.00235335500776368));
#30335=CARTESIAN_POINT('',(0.00563806590144799,-0.00458467403753809,-0.00228113967672));
#30336=CARTESIAN_POINT('',(0.00489201581527501,-0.00537372737396127,-0.00224470719243486));
#30337=CARTESIAN_POINT('',(0.00313715298830232,-0.00655503508824093,-0.00217254587986231));
#30338=CARTESIAN_POINT('',(0.00212524786670617,-0.00694907362059226,-0.00213611317368258));
#30339=CARTESIAN_POINT('',(3.34990726649879E-5,-0.00726733745111344,-0.00206389837896573));
#30340=CARTESIAN_POINT('',(-0.0010491364390756,-0.00719074784021935,-0.00202755451983032));
#30341=CARTESIAN_POINT('',(-0.00307736969557517,-0.00658408658164341,-0.00195517989390222));
#30342=CARTESIAN_POINT('',(-0.00402230947970432,-0.00605261991751492,-0.00191901194879282));
#30343=CARTESIAN_POINT('',(-0.00559778534343856,-0.00463550142938151,-0.00184637479756761));
#30344=CARTESIAN_POINT('',(-0.00622409311108227,-0.00375286918367897,-0.00181046543835526));
#30345=CARTESIAN_POINT('',(-0.00704258456040493,-0.00179513925006642,-0.00173746982761822));
#30346=CARTESIAN_POINT('',(-0.00723127223232795,-0.000729484790167686,-0.00170156076280402));
#30347=CARTESIAN_POINT('',(-0.00713350860255669,0.001387303147611,-0.00162892288212461));
#30348=CARTESIAN_POINT('',(-0.00684827074845186,0.00243321120648628,-0.00159275558730857));
#30349=CARTESIAN_POINT('',(-0.00585576622975641,0.00430315844719611,-0.00152038011254261));
#30350=CARTESIAN_POINT('',(-0.00514991209723177,0.00512758188780289,-0.00148403682594472));
#30351=CARTESIAN_POINT('',(-0.00345441489233604,0.00639328091758393,-0.0014118214949026));
#30352=CARTESIAN_POINT('',(-0.00246319684839593,0.00683677013746831,-0.00137538901060983));
#30353=CARTESIAN_POINT('',(-0.000389848109407185,0.00725659922634024,-0.00130322769805111));
#30354=CARTESIAN_POINT('',(0.000695822339321743,0.0072334040362362,-0.00126679499186096));
#30355=CARTESIAN_POINT('',(0.00275014053235359,0.00672696386704615,-0.00119458019715104));
#30356=CARTESIAN_POINT('',(0.00372105574764232,0.00624189761950416,-0.00115823633801324));
#30357=CARTESIAN_POINT('',(0.00536273972776455,0.00490524443530179,-0.00108586171208286));
#30358=CARTESIAN_POINT('',(0.00603236676655764,0.00405262046213594,-0.00104969376697167));
#30359=CARTESIAN_POINT('',(0.00694560890392401,0.00214046518466646,-0.000977056615752623));
#30360=CARTESIAN_POINT('',(0.00718647309420243,0.00108534171188339,-0.000941147256542428));
#30361=CARTESIAN_POINT('',(0.00719346978112524,-0.00103658802115264,-0.000868151645794657));
#30362=CARTESIAN_POINT('',(0.00695998615282431,-0.00209333201131553,-0.000832242580984424));
#30363=CARTESIAN_POINT('',(0.0060596046626397,-0.00401157654029634,-0.000759604700308071));
#30364=CARTESIAN_POINT('',(0.00539582756142148,-0.00486871378773222,-0.00072343740548999));
#30365=CARTESIAN_POINT('',(0.00376327512225938,-0.00621650473444972,-0.000651061930724788));
#30366=CARTESIAN_POINT('',(0.00279565774430887,-0.00670805399516193,-0.000614718644124706));
#30367=CARTESIAN_POINT('',(0.000744860530219189,-0.00722856873316375,-0.000542503313086405));
#30368=CARTESIAN_POINT('',(-0.000340621509718041,-0.00725897662302607,-0.000506070828791677));
#30369=CARTESIAN_POINT('',(-0.00241680761016381,-0.00685341191346234,-0.000433909516232949));
#30370=CARTESIAN_POINT('',(-0.00341095990183245,-0.00641651425833751,-0.000397476810045951));
#30371=CARTESIAN_POINT('',(-0.00511509617140642,-0.00516247101429958,-0.000325262015329883));
#30372=CARTESIAN_POINT('',(-0.00582647805008241,-0.00434277506916021,-0.000288918156194358));
#30373=CARTESIAN_POINT('',(-0.00683168124975823,-0.00247962328984105,-0.000216543530265495));
#30374=CARTESIAN_POINT('',(-0.00712405089674981,-0.00143564627849449,-0.000180375585155457));
#30375=CARTESIAN_POINT('',(-0.00723602647088685,0.000680437481053904,-0.000107738433932561));
#30376=CARTESIAN_POINT('',(-0.00705477769426858,0.00174741919689845,-7.18290747204408E-5));
#30377=CARTESIAN_POINT('',(-0.00624921443663745,0.00371050416284529,1.1665360196661E-6));
#30378=CARTESIAN_POINT('',(-0.00562910527398621,0.00459745799018268,3.70756008341184E-5));
#30379=CARTESIAN_POINT('',(-0.00406318084328683,0.00602512376975562,0.000109713481509706));
#30380=CARTESIAN_POINT('',(-0.00312191854146526,0.0065629988297973,0.000145880776325484));
#30381=CARTESIAN_POINT('',(-0.00109785949157093,0.00718344452863693,0.000218256251096054));
#30382=CARTESIAN_POINT('',(-1.57898425130279E-5,0.0072672856904212,0.00025459953768962));
#30383=CARTESIAN_POINT('',(0.00207809209544763,0.00696337248625816,0.000326814868735592));
#30384=CARTESIAN_POINT('',(0.00309258333071925,0.0065760697205136,0.000363247353026133));
#30385=CARTESIAN_POINT('',(0.00485552627950401,0.00540685476309468,0.000435408665585627));
#30386=CARTESIAN_POINT('',(0.00560680973971897,0.00462276835045254,0.000471841371774156));
#30387=CARTESIAN_POINT('',(0.00670132478682792,0.00281203874754161,0.000544056166486389));
#30388=CARTESIAN_POINT('',(0.00704487188655321,0.00178250438189151,0.000580400025623436));
#30389=CARTESIAN_POINT('',(0.00726056123082148,-0.000323498023658519,0.000652774651553067));
#30390=CARTESIAN_POINT('',(0.00713116285759123,-0.00139989203688551,0.000688942596660811));
#30391=CARTESIAN_POINT('',(0.00642482460240361,-0.00339774970846239,0.000761579747887542));
#30392=CARTESIAN_POINT('',(0.00584905634210076,-0.00431415137334655,0.000797489107096591));
#30393=CARTESIAN_POINT('',(0.00435357284344211,-0.00581952968154928,0.000870484717838998));
#30394=CARTESIAN_POINT('',(0.00344124414514933,-0.00640166266610323,0.000906393782650393));
#30395=CARTESIAN_POINT('',(0.00144817457336979,-0.0071214005231543,0.000979031663329816));
#30396=CARTESIAN_POINT('',(0.000372725723832011,-0.00725812679375817,0.00101519895814289));
#30397=CARTESIAN_POINT('',(-0.00173469529458699,-0.00705677001142606,0.001087574432915));
#30398=CARTESIAN_POINT('',(-0.00276648191966839,-0.00672013901742019,0.00112391771951012));
#30399=CARTESIAN_POINT('',(-0.00458467403753602,-0.00563806590145063,0.00119613305055149));
#30400=CARTESIAN_POINT('',(-0.00537372737395561,-0.00489201581527777,0.0012325655348454));
#30401=CARTESIAN_POINT('',(-0.00655503508824468,-0.00313715298830325,0.00130472684740259));
#30402=CARTESIAN_POINT('',(-0.00694907362059189,-0.00212524786670655,0.00134115955359244));
#30403=CARTESIAN_POINT('',(-0.00726733745111301,-3.34990726660305E-5,0.00141337434830467));
#30404=CARTESIAN_POINT('',(-0.00719074784021694,0.00104913643907056,0.00144971820744406));
#30405=CARTESIAN_POINT('',(-0.00658408658164684,0.00307736969556589,0.00152209283336755));
#30406=CARTESIAN_POINT('',(-0.00605261991753943,0.00402230947972834,0.00155826077848144));
#30407=CARTESIAN_POINT('',(-0.00463550142931737,0.00559778534347777,0.00163089792971939));
#30408=CARTESIAN_POINT('',(-0.00375286918359511,0.006224093110923,0.00166680728882057));
#30409=CARTESIAN_POINT('',(-0.00179513925064184,0.00704258456042806,0.00173980289960575));
#30410=CARTESIAN_POINT('',(-0.0007294847893921,0.00723127223276442,0.00177571196536462));
#30411=CARTESIAN_POINT('',(0.00138730314952183,0.00713350860123271,0.00184834984465922));
#30412=CARTESIAN_POINT('',(0.00243321120190955,0.00684827075054466,0.00188451713634817));
#30413=CARTESIAN_POINT('',(0.00430315844327975,0.00585576623654509,0.00195689261891401));
#30414=CARTESIAN_POINT('',(0.00512758189718962,0.00514991207766484,0.00199323591196856));
#30415=CARTESIAN_POINT('',(0.00639328092669331,0.00345441487247999,0.00206545120685874));
#30416=CARTESIAN_POINT('',(0.00683677013791915,0.00246319691575483,0.00210188370012292));
#30417=CARTESIAN_POINT('',(0.00725659916989426,0.000389848177144325,0.0021740451558294));
#30418=CARTESIAN_POINT('',(0.00723340408349491,-0.00069582248149021,0.00221047768728494));
#30419=CARTESIAN_POINT('',(0.00672696408575062,-0.00275014098145917,0.00228269199671924));
#30420=CARTESIAN_POINT('',(0.00624189664462071,-0.00372105507060881,0.00231903694593017));
#30421=CARTESIAN_POINT('',(0.00490524509323122,-0.00536273718611709,0.00239141293832608));
#30422=CARTESIAN_POINT('',(0.00405262592252595,-0.00603237309137095,0.00242757601191714));
#30423=CARTESIAN_POINT('',(0.00214045155004707,-0.00694561550063064,0.00250021030746631));
#30424=CARTESIAN_POINT('',(0.00108533037484742,-0.00718642631050035,0.00253615220355904));
#30425=CARTESIAN_POINT('',(-0.00186165676778948,-0.00719625441939621,0.00263749534989383));
#30426=CARTESIAN_POINT('',(-0.00372887586619293,-0.00642951945250147,0.00270113018670128));
#30427=CARTESIAN_POINT('',(-0.00640422907181245,-0.00377360050585877,0.00283056960872658));
#30428=CARTESIAN_POINT('',(-0.00718374672632692,-0.00190268100220303,0.00289444373919848));
#30429=CARTESIAN_POINT('',(-0.00718994287258576,-2.43759101863917E-5,0.00295904411866391));
#30430=CARTESIAN_POINT('',(-0.006,-2.43712308653931E-5,-0.0140410700265819));
#30431=CARTESIAN_POINT('',(-0.00600309747414711,0.000755994738560391,-0.0140090793492257));
#30432=CARTESIAN_POINT('',(-0.00585022549906422,0.00154554847924553,-0.0139767317091225));
#30433=CARTESIAN_POINT('',(-0.00488277416170381,0.00391156551240249,-0.0138719117580559));
#30434=CARTESIAN_POINT('',(-0.00345414811439852,0.00521522772168569,-0.0137995939835592));
#30435=CARTESIAN_POINT('',(-0.000920416913494161,0.00599387797088215,-0.0136909247186258));
#30436=CARTESIAN_POINT('',(-1.83364399790589E-5,0.00606458475875607,-0.0136547070017816));
#30437=CARTESIAN_POINT('',(0.00173071508355203,0.00581192078991974,-0.013582263622242));
#30438=CARTESIAN_POINT('',(0.00257620709021928,0.0054899026401681,-0.013546041378497));
#30439=CARTESIAN_POINT('',(0.0040496481570146,0.00451412616898593,-0.0134735982934369));
#30440=CARTESIAN_POINT('',(0.00467595743139725,0.00386119227478036,-0.0134373767382566));
#30441=CARTESIAN_POINT('',(0.00559115533267521,0.00234942868328478,-0.0133649337688717));
#30442=CARTESIAN_POINT('',(0.00587789190074464,0.00149118187026969,-0.013328711875432));
#30443=CARTESIAN_POINT('',(0.00605911477020831,-0.000266602851011457,-0.0132562691328768));
#30444=CARTESIAN_POINT('',(0.00595132195371268,-0.00116523586494131,-0.0132200472158988));
#30445=CARTESIAN_POINT('',(0.00536345211542811,-0.00283155473315956,-0.0131476043990316));
#30446=CARTESIAN_POINT('',(0.00488207572844726,-0.00359821831670739,-0.013111382654392));
#30447=CARTESIAN_POINT('',(0.00363763601600018,-0.00485255191712249,-0.0130389394867723));
#30448=CARTESIAN_POINT('',(0.00287504504636738,-0.00534029243914702,-0.0130027180351518));
#30449=CARTESIAN_POINT('',(0.00121351369399411,-0.00594156052931282,-0.0129302744931486));
#30450=CARTESIAN_POINT('',(0.000315825750312525,-0.00605668045304735,-0.0128940532261725));
#30451=CARTESIAN_POINT('',(-0.00144337707403964,-0.00588978902230696,-0.0128216096183549));
#30452=CARTESIAN_POINT('',(-0.00230387638883705,-0.00560996798125232,-0.012785388316591));
#30453=CARTESIAN_POINT('',(-0.00382310259116674,-0.00470721006652816,-0.0127129448611614));
#30454=CARTESIAN_POINT('',(-0.00448099997246373,-0.00408613400852397,-0.0126767233862572));
#30455=CARTESIAN_POINT('',(-0.0054688674143523,-0.00262077375144199,-0.0126042801976742));
#30456=CARTESIAN_POINT('',(-0.00579763556460296,-0.0017778661740937,-0.0125680585008892));
#30457=CARTESIAN_POINT('',(-0.00606464167597128,-3.0946622266283E-5,-0.0124956155817382));
#30458=CARTESIAN_POINT('',(-0.00600111463142179,0.00087169976698755,-0.012459393707512));
#30459=CARTESIAN_POINT('',(-0.00549586755061847,0.00256503164149849,-0.0123869509484387));
#30460=CARTESIAN_POINT('',(-0.0050523880893689,0.00335400980216192,-0.0123507290311181));
#30461=CARTESIAN_POINT('',(-0.00387159456299549,0.00466851979026504,-0.0122782862186558));
#30462=CARTESIAN_POINT('',(-0.00313347130157478,0.00519260976096335,-0.0122420644730658));
#30463=CARTESIAN_POINT('',(-0.00150374624037729,0.00587523641666246,-0.0121696213045038));
#30464=CARTESIAN_POINT('',(-0.000612553833171288,0.00603401898911306,-0.0121333998532844));
#30465=CARTESIAN_POINT('',(0.00115259631366971,0.00595367775238322,-0.012060956311437));
#30466=CARTESIAN_POINT('',(0.00202600631780663,0.00571650438740237,-0.0120247350443508));
#30467=CARTESIAN_POINT('',(0.00358743121515774,0.00488909903514313,-0.0119522914365147));
#30468=CARTESIAN_POINT('',(0.00427534604366821,0.00430127927179916,-0.0119160701347756));
#30469=CARTESIAN_POINT('',(0.00533345753982393,0.00288585701390729,-0.011843626679348));
#30470=CARTESIAN_POINT('',(0.00570359994722143,0.00206029112764935,-0.0118074052044376));
#30471=CARTESIAN_POINT('',(0.00605550136478055,0.000328434275013915,-0.0117349620158554));
#30472=CARTESIAN_POINT('',(0.00603667676489193,-0.000576124907669123,-0.0116987403190736));
#30473=CARTESIAN_POINT('',(0.00561484107606885,-0.00229224694171357,-0.0116262973999176));
#30474=CARTESIAN_POINT('',(0.00521072192138963,-0.00310187271837801,-0.0115900755256951));
#30475=CARTESIAN_POINT('',(0.0040959244307272,-0.0044729576919261,-0.0115176327666191));
#30476=CARTESIAN_POINT('',(0.0033842739627938,-0.00503216622374487,-0.0114814108492998));
#30477=CARTESIAN_POINT('',(0.00179032179752591,-0.00579474497744012,-0.0114089680368375));
#30478=CARTESIAN_POINT('',(0.000907824274980536,-0.0059964734313809,-0.0113727462912467));
#30479=CARTESIAN_POINT('',(-0.000859075264311106,-0.00600346944668868,-0.0113003031226866));
#30480=CARTESIAN_POINT('',(-0.00174319314868272,-0.00580912084620773,-0.0112640816714646));
#30481=CARTESIAN_POINT('',(-0.00334323398092842,-0.00505940150515071,-0.0111916381296202));
#30482=CARTESIAN_POINT('',(-0.0040593972898715,-0.00450604234934652,-0.0111554168625309));
#30483=CARTESIAN_POINT('',(-0.00518533147390755,-0.00314408804019317,-0.0110829732546983));
#30484=CARTESIAN_POINT('',(-0.00559593301943456,-0.00233775978428837,-0.0110467519529574));
#30485=CARTESIAN_POINT('',(-0.00603184192596513,-0.000625158391190649,-0.0109743084975298));
#30486=CARTESIAN_POINT('',(-0.00605787853325042,0.000279212400784205,-0.010938087022621));
#30487=CARTESIAN_POINT('',(-0.00572024012570424,0.00201390634250815,-0.0108656438340358));
#30488=CARTESIAN_POINT('',(-0.00535668865032753,0.00284240619482864,-0.0108294221372547));
#30489=CARTESIAN_POINT('',(-0.00431023182100595,0.00426646668808826,-0.0107569792181002));
#30490=CARTESIAN_POINT('',(-0.00362704403416047,0.0048598136669573,-0.0107207573438761));
#30491=CARTESIAN_POINT('',(-0.00207241394588092,0.00569991648120368,-0.0106483145848017));
#30492=CARTESIAN_POINT('',(-0.00120093480390402,0.00594422095445996,-0.0106120926674817));
#30493=CARTESIAN_POINT('',(0.000563511232301897,0.00603877277129276,-0.0105396498550195));
#30494=CARTESIAN_POINT('',(0.00145603076803849,0.00588742838004165,-0.01050342810943));
#30495=CARTESIAN_POINT('',(0.003091110347539,0.0052177286750386,-0.0104309849408669));
#30496=CARTESIAN_POINT('',(0.00383355477573361,0.00469983671428884,-0.0103947634896458));
#30497=CARTESIAN_POINT('',(0.00502489458107504,0.00339487724234225,-0.0103223199478029));
#30498=CARTESIAN_POINT('',(0.00547478182306626,0.00260957621096752,-0.0102860986807135));
#30499=CARTESIAN_POINT('',(0.00599381202091714,0.000920418142363337,-0.0102136550728794));
#30500=CARTESIAN_POINT('',(0.00606458992024415,1.83375614756708E-5,-0.0101774337711432));
#30501=CARTESIAN_POINT('',(0.00581193305766793,-0.00173071492951537,-0.0101049903157079));
#30502=CARTESIAN_POINT('',(0.00548990002742215,-0.00257620837226416,-0.0100687688408028));
#30503=CARTESIAN_POINT('',(0.00451412418157153,-0.00404964797549366,-0.00999632565221761));
#30504=CARTESIAN_POINT('',(0.00386119324725615,-0.00467595690529434,-0.00996010395543582));
#30505=CARTESIAN_POINT('',(0.00234942884354364,-0.00559115555682603,-0.00988766103628286));
#30506=CARTESIAN_POINT('',(0.00149118157195093,-0.00587789203903946,-0.00985143916205724));
#30507=CARTESIAN_POINT('',(-0.000266602775728381,-0.00605911465611149,-0.00977899640298428));
#30508=CARTESIAN_POINT('',(-0.00116523579238055,-0.00595132192935385,-0.00974277448566356));
#30509=CARTESIAN_POINT('',(-0.0028315547852557,-0.00536345215233157,-0.00967033167320129));
#30510=CARTESIAN_POINT('',(-0.00359821832558892,-0.00488207572751732,-0.00963410992760799));
#30511=CARTESIAN_POINT('',(-0.00485255190132513,-0.00363763601143704,-0.00956166675905256));
#30512=CARTESIAN_POINT('',(-0.00534029243944068,-0.00287504504673827,-0.00952544530782837));
#30513=CARTESIAN_POINT('',(-0.00594156053203977,-0.00121351369403066,-0.00945300176598398));
#30514=CARTESIAN_POINT('',(-0.00605668045273713,-0.000315825750337319,-0.00941678049889378));
#30515=CARTESIAN_POINT('',(-0.00588978902176606,0.00144337707403134,-0.00934433689106272));
#30516=CARTESIAN_POINT('',(-0.00560996798134601,0.00230387638883739,-0.0093081155893231));
#30517=CARTESIAN_POINT('',(-0.00470721006664119,0.00382310259118043,-0.00923567213389156));
#30518=CARTESIAN_POINT('',(-0.00408613400847974,0.00448099997245,-0.00919945065898276));
#30519=CARTESIAN_POINT('',(-0.0026207737514388,0.00546886741436465,-0.00912700747040132));
#30520=CARTESIAN_POINT('',(-0.00177786617410126,0.00579763556459996,-0.00909078577361959));
#30521=CARTESIAN_POINT('',(-3.09466222681958E-5,0.00606464167597443,-0.00901834285446272));
#30522=CARTESIAN_POINT('',(0.000871699766989816,0.00600111463142254,-0.00898212098023906));
#30523=CARTESIAN_POINT('',(0.00256503164149829,0.00549586755061753,-0.0089096782211661));
#30524=CARTESIAN_POINT('',(0.00335400980216468,0.00505238808937253,-0.00887345630384614));
#30525=CARTESIAN_POINT('',(0.00466851979026242,0.00387159456299146,-0.00880101349138235));
#30526=CARTESIAN_POINT('',(0.00519260976097037,0.0031334713015793,-0.00876479174579288));
#30527=CARTESIAN_POINT('',(0.00587523641665553,0.00150374624037253,-0.00869234857723131));
#30528=CARTESIAN_POINT('',(0.0060340189891069,0.000612553833172357,-0.00865612712601019));
#30529=CARTESIAN_POINT('',(0.00595367775238934,-0.00115259631367031,-0.00858368358416579));
#30530=CARTESIAN_POINT('',(0.0057165043874037,-0.00202600631780788,-0.00854746231707637));
#30531=CARTESIAN_POINT('',(0.00488909903514167,-0.00358743121515669,-0.00847501870924377));
#30532=CARTESIAN_POINT('',(0.00430127927179329,-0.00427534604365617,-0.00843879740750493));
#30533=CARTESIAN_POINT('',(0.00288585701391485,-0.00533345753983467,-0.00836635395207338));
#30534=CARTESIAN_POINT('',(0.0020602911276489,-0.00570359994720765,-0.00833013247716457));
#30535=CARTESIAN_POINT('',(0.000328434275016982,-0.00605550136479379,-0.00825768928858313));
#30536=CARTESIAN_POINT('',(-0.000576124907666656,-0.00603667676488749,-0.00822146759180141));
#30537=CARTESIAN_POINT('',(-0.00229224694171241,-0.00561484107607418,-0.00814902467264454));
#30538=CARTESIAN_POINT('',(-0.00310187271838032,-0.00521072192139484,-0.00811280279842165));
#30539=CARTESIAN_POINT('',(-0.004472957691924,-0.00409592443072183,-0.00804036003934715));
#30540=CARTESIAN_POINT('',(-0.00503216622374263,-0.00338427396279622,-0.00800413812202796));
#30541=CARTESIAN_POINT('',(-0.00579474497744008,-0.00179032179752817,-0.00793169530956417));
#30542=CARTESIAN_POINT('',(-0.00599647343138397,-0.000907824274979786,-0.00789547356397393));
#30543=CARTESIAN_POINT('',(-0.00600346944668562,0.000859075264311016,-0.00782303039541389));
#30544=CARTESIAN_POINT('',(-0.00580912084621274,0.0017431931486827,-0.00778680894419278));
#30545=CARTESIAN_POINT('',(-0.00505940150514794,0.00334323398092366,-0.00771436540234685));
#30546=CARTESIAN_POINT('',(-0.00450604234934851,0.00405939728987541,-0.00767814413525819));
#30547=CARTESIAN_POINT('',(-0.00314408804019073,0.00518533147390397,-0.00760570052742559));
#30548=CARTESIAN_POINT('',(-0.00233775978429126,0.00559593301943496,-0.00756947922568675));
#30549=CARTESIAN_POINT('',(-0.000625158391191966,0.00603184192596372,-0.00749703577025521));
#30550=CARTESIAN_POINT('',(0.000279212400785439,0.00605787853325739,-0.0074608142953487));
#30551=CARTESIAN_POINT('',(0.00201390634250682,0.0057202401256973,-0.00738837110676266));
#30552=CARTESIAN_POINT('',(0.00284240619482905,0.00535668865032929,-0.0073521494099817));
#30553=CARTESIAN_POINT('',(0.00426646668808612,0.00431023182100547,-0.0072797064908279));
#30554=CARTESIAN_POINT('',(0.00485981366694846,0.00362704403415547,-0.00724348461660347));
#30555=CARTESIAN_POINT('',(0.00569991648121184,0.00207241394588719,-0.00717104185752897));
#30556=CARTESIAN_POINT('',(0.00594422095445765,0.00120093480390459,-0.00713481994020902));
#30557=CARTESIAN_POINT('',(0.00603877277129507,-0.00056351123230199,-0.00706237712774675));
#30558=CARTESIAN_POINT('',(0.0058874283800451,-0.00145603076804085,-0.0070261553821569));
#30559=CARTESIAN_POINT('',(0.00521772867503515,-0.00309111034753677,-0.00695371221359457));
#30560=CARTESIAN_POINT('',(0.00469983671428812,-0.00383355477573512,-0.006917490762375));
#30561=CARTESIAN_POINT('',(0.00339487724234326,-0.00502489458107331,-0.00684504722052831));
#30562=CARTESIAN_POINT('',(0.00260957621096805,-0.00547478182307112,-0.00680882595343965));
#30563=CARTESIAN_POINT('',(0.00092041814236392,-0.00599381202091195,-0.00673638234560783));
#30564=CARTESIAN_POINT('',(1.83375614742641E-5,-0.00606458992025192,-0.00670016104386784));
#30565=CARTESIAN_POINT('',(-0.00173071492951204,-0.00581193305766056,-0.00662771758843784));
#30566=CARTESIAN_POINT('',(-0.00257620837226887,-0.00548990002742911,-0.00659149611352898));
#30567=CARTESIAN_POINT('',(-0.00404964797548944,-0.00451412418156432,-0.00651905292494602));
#30568=CARTESIAN_POINT('',(-0.00467595690530402,-0.00386119324726373,-0.00648283122816474));
#30569=CARTESIAN_POINT('',(-0.00559115555681467,-0.002349428843539,-0.00641038830900865));
#30570=CARTESIAN_POINT('',(-0.00587789203904983,-0.00149118157195279,-0.00637416643478492));
#30571=CARTESIAN_POINT('',(-0.00605911465610112,0.000266602775729709,-0.0063017236757112));
#30572=CARTESIAN_POINT('',(-0.0059513219293497,0.00116523579237788,-0.00626550175839094));
#30573=CARTESIAN_POINT('',(-0.00536345215233749,0.00283155478525354,-0.00619305894592869));
#30574=CARTESIAN_POINT('',(-0.0048820757275079,0.00359821832558035,-0.00615683720033756));
#30575=CARTESIAN_POINT('',(-0.00363763601144603,0.0048525519013342,-0.00608439403177752));
#30576=CARTESIAN_POINT('',(-0.00287504504674204,0.00534029243944514,-0.00604817258055424));
#30577=CARTESIAN_POINT('',(-0.00121351369403187,0.00594156053203358,-0.0059757290387129));
#30578=CARTESIAN_POINT('',(-0.00031582575033843,0.00605668045273254,-0.00593950777162106));
#30579=CARTESIAN_POINT('',(0.00144337707403289,0.00588978902177064,-0.00586706416378998));
#30580=CARTESIAN_POINT('',(0.00230387638884796,0.00560996798136351,-0.00583084286204893));
#30581=CARTESIAN_POINT('',(0.00382310259116669,0.00470721006662557,-0.00575839940662044));
#30582=CARTESIAN_POINT('',(0.00448099997245725,0.00408613400848599,-0.0057221779317101));
#30583=CARTESIAN_POINT('',(0.00546886741435594,0.00262077375143485,-0.00564973474312865));
#30584=CARTESIAN_POINT('',(0.00579763556459787,0.00177786617410278,-0.00561351304634461));
#30585=CARTESIAN_POINT('',(0.00606464167597621,3.0946622268693E-5,-0.00554107012719234));
#30586=CARTESIAN_POINT('',(0.00600111463141991,-0.000871699766989554,-0.0055048482529664));
#30587=CARTESIAN_POINT('',(0.00549586755062006,-0.00256503164149915,-0.0054324054938933));
#30588=CARTESIAN_POINT('',(0.00505238808936695,-0.00335400980216068,-0.00539618357657267));
#30589=CARTESIAN_POINT('',(0.00387159456299719,-0.00466851979026632,-0.00532374076411039));
#30590=CARTESIAN_POINT('',(0.00313347130158231,-0.00519260976097808,-0.00528751901851862));
#30591=CARTESIAN_POINT('',(0.00150374624036927,-0.00587523641664796,-0.00521507584996011));
#30592=CARTESIAN_POINT('',(0.000612553833171035,-0.00603401898911497,-0.00517885439873749));
#30593=CARTESIAN_POINT('',(-0.00115259631366817,-0.00595367775238131,-0.0051064108568931));
#30594=CARTESIAN_POINT('',(-0.00202600631781078,-0.00571650438740787,-0.00507018958980372));
#30595=CARTESIAN_POINT('',(-0.00358743121515375,-0.00488909903513752,-0.00499774598197099));
#30596=CARTESIAN_POINT('',(-0.00427534604366103,-0.00430127927179586,-0.00496152468023219));
#30597=CARTESIAN_POINT('',(-0.00533345753983033,-0.00288585701391166,-0.00488908122480065));
#30598=CARTESIAN_POINT('',(-0.00570359994720922,-0.00206029112764941,-0.00485285974989415));
#30599=CARTESIAN_POINT('',(-0.00605550136479229,-0.000328434275016135,-0.00478041656130811));
#30600=CARTESIAN_POINT('',(-0.00603667676488204,0.000576124907666373,-0.00474419486452637));
#30601=CARTESIAN_POINT('',(-0.00561484107607947,0.00229224694171347,-0.00467175194537411));
#30602=CARTESIAN_POINT('',(-0.00521072192140026,0.00310187271838521,-0.00463553007114899));
#30603=CARTESIAN_POINT('',(-0.00409592443071614,0.00447295769191944,-0.00456308731207436));
#30604=CARTESIAN_POINT('',(-0.00338427396279826,0.00503216622374612,-0.00452686539475448));
#30605=CARTESIAN_POINT('',(-0.00179032179752601,0.00579474497743666,-0.00445442258229221));
#30606=CARTESIAN_POINT('',(-0.000907824274979335,0.0059964734313974,-0.00441820083669967));
#30607=CARTESIAN_POINT('',(0.00085907526431096,0.00600346944667221,-0.0043457576681427));
#30608=CARTESIAN_POINT('',(0.00174319314868342,0.00580912084621372,-0.00430953621691928));
#30609=CARTESIAN_POINT('',(0.00334323398092361,0.00505940150514661,-0.00423709267507489));
#30610=CARTESIAN_POINT('',(0.00405939728986873,0.00450604234934388,-0.00420087140798552));
#30611=CARTESIAN_POINT('',(0.00518533147391094,0.00314408804019501,-0.00412842780015279));
#30612=CARTESIAN_POINT('',(0.00559593301943005,0.00233775978429005,-0.00409220649841479));
#30613=CARTESIAN_POINT('',(0.00603184192596878,0.000625158391192479,-0.00401976304298171));
#30614=CARTESIAN_POINT('',(0.00605787853326322,-0.000279212400785085,-0.00398354156807523));
#30615=CARTESIAN_POINT('',(0.00572024012569162,-0.00201390634250648,-0.00391109837949073));
#30616=CARTESIAN_POINT('',(0.00535668865032563,-0.00284240619482649,-0.0038748766827105));
#30617=CARTESIAN_POINT('',(0.00431023182100872,-0.0042664666880893,-0.00380243376355363));
#30618=CARTESIAN_POINT('',(0.00362704403415923,-0.00485981366695353,-0.00376621188933157));
#30619=CARTESIAN_POINT('',(0.00207241394588276,-0.00569991648120711,-0.0036937691302554));
#30620=CARTESIAN_POINT('',(0.00120093480390449,-0.00594422095445802,-0.00365754721293706));
#30621=CARTESIAN_POINT('',(-0.000563511232301889,-0.00603877277129467,-0.00358510440047326));
#30622=CARTESIAN_POINT('',(-0.00145603076803988,-0.00588742838004119,-0.00354888265488379));
#30623=CARTESIAN_POINT('',(-0.00309111034753821,-0.00521772867503886,-0.00347643948632222));
#30624=CARTESIAN_POINT('',(-0.00383355477573305,-0.00469983671428823,-0.00344021803510188));
#30625=CARTESIAN_POINT('',(-0.005024894581076,-0.00339487724234243,-0.00336777449325594));
#30626=CARTESIAN_POINT('',(-0.00547478182306962,-0.00260957621096737,-0.00333155322616581));
#30627=CARTESIAN_POINT('',(-0.00599381202091404,-0.000920418142362637,-0.00325910961833615));
#30628=CARTESIAN_POINT('',(-0.00606458992025173,-1.83375614733508E-5,-0.00322288831659661));
#30629=CARTESIAN_POINT('',(-0.00581193305766033,0.00173071492951357,-0.00315044486116353));
#30630=CARTESIAN_POINT('',(-0.00548990002742595,0.00257620837226724,-0.00311422338625548));
#30631=CARTESIAN_POINT('',(-0.00451412418156716,0.00404964797549147,-0.00304178019767404));
#30632=CARTESIAN_POINT('',(-0.00386119324726109,0.00467595690530463,-0.00300555850089079));
#30633=CARTESIAN_POINT('',(-0.00234942884353807,0.00559115555681618,-0.00293311558173699));
#30634=CARTESIAN_POINT('',(-0.00149118157195182,0.00587789203904661,-0.00289689370751264));
#30635=CARTESIAN_POINT('',(0.000266602775729427,0.0060591146561044,-0.00282445094843801));
#30636=CARTESIAN_POINT('',(0.00116523579237932,0.00595132192934975,-0.00278822903111813));
#30637=CARTESIAN_POINT('',(0.00283155478525638,0.00536345215233592,-0.00271578621865587));
#30638=CARTESIAN_POINT('',(0.00359821832558002,0.00488207572750747,-0.00267956447306408));
#30639=CARTESIAN_POINT('',(0.00485255190133472,0.00363763601144627,-0.00260712130450557));
#30640=CARTESIAN_POINT('',(0.00534029243944329,0.0028750450467383,-0.00257089985328367));
#30641=CARTESIAN_POINT('',(0.00594156053203786,0.00121351369402893,-0.00249845631143773));
#30642=CARTESIAN_POINT('',(0.00605668045272946,0.00031582575033894,-0.00246223504434917));
#30643=CARTESIAN_POINT('',(0.00588978902177369,-0.00144337707403387,-0.00238979143651642));
#30644=CARTESIAN_POINT('',(0.00560996798136092,-0.00230387638884949,-0.00235357013477837));
#30645=CARTESIAN_POINT('',(0.00470721006662452,-0.00382310259117127,-0.00228112667934528));
#30646=CARTESIAN_POINT('',(0.00408613400848635,-0.00448099997246406,-0.00224490520443801));
#30647=CARTESIAN_POINT('',(0.00262077375142909,-0.00546886741435278,-0.00217246201585504));
#30648=CARTESIAN_POINT('',(0.00177786617409953,-0.00579763556459878,-0.00213624031907329));
#30649=CARTESIAN_POINT('',(3.09466222649569E-5,-0.00606464167597636,-0.00206379739991795));
#30650=CARTESIAN_POINT('',(-0.000871699766989641,-0.00600111463142063,-0.00202757552569444));
#30651=CARTESIAN_POINT('',(-0.0025650316414994,-0.00549586755061925,-0.00195513276661981));
#30652=CARTESIAN_POINT('',(-0.00335400980216594,-0.0050523880893681,-0.00191891084930058));
#30653=CARTESIAN_POINT('',(-0.00466851979026617,-0.00387159456299146,-0.00184646803683676));
#30654=CARTESIAN_POINT('',(-0.00519260976097701,-0.00313347130158175,-0.0018102462912459));
#30655=CARTESIAN_POINT('',(-0.00587523641664912,-0.00150374624036962,-0.0017378031226874));
#30656=CARTESIAN_POINT('',(-0.00603401898911557,-0.00061255383316749,-0.00170158167146463));
#30657=CARTESIAN_POINT('',(-0.00595367775238039,0.00115259631367158,-0.00162913812962024));
#30658=CARTESIAN_POINT('',(-0.00571650438740898,0.00202600631781163,-0.00159291686253176));
#30659=CARTESIAN_POINT('',(-0.00488909903513646,0.00358743121515282,-0.00152047325469751));
#30660=CARTESIAN_POINT('',(-0.0043012792717929,0.0042753460436607,-0.00148425195295939));
#30661=CARTESIAN_POINT('',(-0.00288585701391163,0.00533345753983288,-0.00141180849752786));
#30662=CARTESIAN_POINT('',(-0.00206029112764908,0.00570359994721081,-0.00137558702261988));
#30663=CARTESIAN_POINT('',(-0.000328434275016096,0.00605550136479076,-0.00130314383403692));
#30664=CARTESIAN_POINT('',(0.000576124907667665,0.00603667676488167,-0.00126692213725589));
#30665=CARTESIAN_POINT('',(0.00229224694171486,0.00561484107607917,-0.00119447921809904));
#30666=CARTESIAN_POINT('',(0.00310187271838672,0.00521072192140026,-0.00115825734387622));
#30667=CARTESIAN_POINT('',(0.00447295769191957,0.00409592443071479,-0.00108581458480161));
#30668=CARTESIAN_POINT('',(0.00503216622374031,0.00338427396279337,-0.00104959266748173));
#30669=CARTESIAN_POINT('',(0.005794744977443,0.0017903217975298,-0.000977149855019475));
#30670=CARTESIAN_POINT('',(0.00599647343139357,0.000907824274979128,-0.000940928109428471));
#30671=CARTESIAN_POINT('',(0.00600346944667604,-0.000859075264311266,-0.000868484940868442));
#30672=CARTESIAN_POINT('',(0.00580912084621264,-0.0017431931486827,-0.0008322634896458));
#30673=CARTESIAN_POINT('',(0.00505940150514784,-0.00334323398092403,-0.000759819947802938));
#30674=CARTESIAN_POINT('',(0.00450604234934318,-0.00405939728986845,-0.000723598680712034));
#30675=CARTESIAN_POINT('',(0.00314408804019546,-0.00518533147391142,-0.000651155072880834));
#30676=CARTESIAN_POINT('',(0.00233775978428977,-0.00559593301942972,-0.000614933771140532));
#30677=CARTESIAN_POINT('',(0.000625158391192401,-0.00603184192596921,-0.000542490315710523));
#30678=CARTESIAN_POINT('',(-0.000279212400785806,-0.00605787853326039,-0.000506268840800958));
#30679=CARTESIAN_POINT('',(-0.00201390634250717,-0.00572024012569417,-0.000433825652219523));
#30680=CARTESIAN_POINT('',(-0.00284240619482663,-0.00535668865032544,-0.000397603955437035));
#30681=CARTESIAN_POINT('',(-0.00426646668808866,-0.0043102318210093,-0.000325161036281701));
#30682=CARTESIAN_POINT('',(-0.00485981366695287,-0.00362704403415734,-0.000288939162058086));
#30683=CARTESIAN_POINT('',(-0.00569991648120799,-0.00207241394588432,-0.000216496402983457));
#30684=CARTESIAN_POINT('',(-0.0059442209544565,-0.00120093480390377,-0.000180274485662048));
#30685=CARTESIAN_POINT('',(-0.00603877277129622,0.000563511232301556,-0.000107831673202851));
#30686=CARTESIAN_POINT('',(-0.00588742838004495,0.00145603076804102,-7.16099276087707E-5));
#30687=CARTESIAN_POINT('',(-0.00521772867503495,0.00309111034753743,8.33240948196383E-7));
#30688=CARTESIAN_POINT('',(-0.00469983671428809,0.00383355477573433,3.70546921731411E-5));
#30689=CARTESIAN_POINT('',(-0.00339487724234229,0.00502489458107499,0.000109498234014469));
#30690=CARTESIAN_POINT('',(-0.00260957621096751,0.00547478182307082,0.000145719501104603));
#30691=CARTESIAN_POINT('',(-0.000920418142362202,0.00599381202091294,0.000218163108938871));
#30692=CARTESIAN_POINT('',(-1.83375614725771E-5,0.00606458992025286,0.00025438441067611));
#30693=CARTESIAN_POINT('',(0.00173071492951319,0.00581193305765916,0.000326827866109187));
#30694=CARTESIAN_POINT('',(0.00257620837226795,0.00548990002742626,0.000363049341015702));
#30695=CARTESIAN_POINT('',(0.00404964797549103,0.0045141241815667,0.000435492529600207));
#30696=CARTESIAN_POINT('',(0.00467595690530011,0.00386119324726,0.000471714226381924));
#30697=CARTESIAN_POINT('',(0.00559115555682087,0.00234942884353889,0.000544157145535723));
#30698=CARTESIAN_POINT('',(0.00587789203904666,0.00149118157195146,0.000580379019759321));
#30699=CARTESIAN_POINT('',(0.00605911465610445,-0.000266602775729979,0.000652821778835484));
#30700=CARTESIAN_POINT('',(0.00595132192935104,-0.0011652357923806,0.000689043696154603));
#30701=CARTESIAN_POINT('',(0.00536345215233414,-0.0028315547852565,0.000761486508616866));
#30702=CARTESIAN_POINT('',(0.00488207572750542,-0.00359821832557824,0.000797708254208643));
#30703=CARTESIAN_POINT('',(0.00363763601144815,-0.00485255190133669,0.000870151422767143));
#30704=CARTESIAN_POINT('',(0.0028750450467372,-0.00534029243944135,0.000906372873988264));
#30705=CARTESIAN_POINT('',(0.00121351369403036,-0.00594156053203968,0.000978816415835729));
#30706=CARTESIAN_POINT('',(0.000315825750338376,-0.00605668045273214,0.00101503768292201));
#30707=CARTESIAN_POINT('',(-0.0014433770740335,-0.00588978902177103,0.00108748129075781));
#30708=CARTESIAN_POINT('',(-0.0023038763888485,-0.00560996798135989,0.00112370259249429));
#30709=CARTESIAN_POINT('',(-0.00382310259117005,-0.0047072100666267,0.00119614604792737));
#30710=CARTESIAN_POINT('',(-0.00448099997246035,-0.00408613400848585,0.00123236752283539));
#30711=CARTESIAN_POINT('',(-0.00546886741435506,-0.00262077375143265,0.00130481071141683));
#30712=CARTESIAN_POINT('',(-0.00579763556459847,-0.0017778661740996,0.00134103240820018));
#30713=CARTESIAN_POINT('',(-0.00606464167597601,-3.09466222654928E-5,0.00141347532735398));
#30714=CARTESIAN_POINT('',(-0.00600111463141992,0.000871699766980109,0.00144969720157956));
#30715=CARTESIAN_POINT('',(-0.00549586755062015,0.00256503164149748,0.00152213996065112));
#30716=CARTESIAN_POINT('',(-0.00505238808936944,0.00335400980220972,0.00155836187797583));
#30717=CARTESIAN_POINT('',(-0.00387159456298909,0.00466851979024306,0.00163080469043323));
#30718=CARTESIAN_POINT('',(-0.00313347130160139,0.00519260976081515,0.00166702643602028));
#30719=CARTESIAN_POINT('',(-0.00150374624037983,0.00587523641686614,0.00173946960459158));
#30720=CARTESIAN_POINT('',(-0.000612553833165579,0.00603401898939451,0.00177569105583878));
#30721=CARTESIAN_POINT('',(0.00115259631371467,0.0059536777513449,0.00184813459759908));
#30722=CARTESIAN_POINT('',(0.00202600631845691,0.00571650438746742,0.00188435586467389));
#30723=CARTESIAN_POINT('',(0.00358743121405334,0.00488909903965777,0.00195679947282889));
#30724=CARTESIAN_POINT('',(0.00427534604012664,0.00430127926719982,0.0019930207743065));
#30725=CARTESIAN_POINT('',(0.00533345754995747,0.00288585699514267,0.00206546422868242));
#30726=CARTESIAN_POINT('',(0.00570359995483104,0.0020602911659135,0.00210168570590789));
#30727=CARTESIAN_POINT('',(0.00605550130478085,0.000328434353748034,0.00217412889706531));
#30728=CARTESIAN_POINT('',(0.00603667678110669,-0.000576125165779344,0.00221035058020653));
#30729=CARTESIAN_POINT('',(0.0056148413322424,-0.00229224724916889,0.00228279349810771));
#30730=CARTESIAN_POINT('',(0.00521072173073282,-0.00310187120641182,0.00231901543922011));
#30731=CARTESIAN_POINT('',(0.00409592363987556,-0.00447295679573389,0.00239145815903209));
#30732=CARTESIAN_POINT('',(0.00338427466196768,-0.00503217385805823,0.00242767978760003));
#30733=CARTESIAN_POINT('',(0.00179032336308774,-0.00579474532206606,0.00250012295961856));
#30734=CARTESIAN_POINT('',(0.000907823357868306,-0.00599643245723689,0.00253634580897236));
#30735=CARTESIAN_POINT('',(-0.00154620346649854,-0.00600624349949343,0.00263695810271456));
#30736=CARTESIAN_POINT('',(-0.00311036825890238,-0.00536525626263524,0.00270138359384264));
#30737=CARTESIAN_POINT('',(-0.00534036428216497,-0.00315440800084661,0.00283011272614596));
#30738=CARTESIAN_POINT('',(-0.005993747924043,-0.00158510314530943,0.00289494802175126));
#30739=CARTESIAN_POINT('',(-0.00599994287806968,-2.43712307521179E-5,0.00295892997067846));
#45463=MECHANICAL_DESIGN_GEOMETRIC_PRESENTATION_REPRESENTATION('',(#13533),#45464);
#45464=(
GEOMETRIC_REPRESENTATION_CONTEXT(3)
GLOBAL_UNCERTAINTY_ASSIGNED_CONTEXT((#45492))
GLOBAL_UNIT_ASSIGNED_CONTEXT((#45522,#45521,#45520))
REPRESENTATION_CONTEXT('MAS-690','TOP_LEVEL_ASSEMBLY_PART')
);
#45469=(
GEOMETRIC_REPRESENTATION_CONTEXT(3)
GLOBAL_UNCERTAINTY_ASSIGNED_CONTEXT((#45497))
GLOBAL_UNIT_ASSIGNED_CONTEXT((#45522,#45521,#45520))
REPRESENTATION_CONTEXT('spring','COMPONENT_PART')
);
#45492=UNCERTAINTY_MEASURE_WITH_UNIT(LENGTH_MEASURE(1.E-8),#45522,
'DISTANCE_ACCURACY_VALUE','Maximum Tolerance applied to model');
#45497=UNCERTAINTY_MEASURE_WITH_UNIT(LENGTH_MEASURE(1.E-8),#45522,
'DISTANCE_ACCURACY_VALUE','Maximum Tolerance applied to model');
#45520=(
NAMED_UNIT(*)
SI_UNIT($,.STERADIAN.)
SOLID_ANGLE_UNIT()
);
#45521=(
NAMED_UNIT(*)
PLANE_ANGLE_UNIT()
SI_UNIT($,.RADIAN.)
);
#45522=(
LENGTH_UNIT()
NAMED_UNIT(*)
SI_UNIT($,.METRE.)
);
#45532=PRODUCT_DEFINITION_SHAPE('','',#45590);
#45590=PRODUCT_DEFINITION('','',#45646,#45618);
#45618=PRODUCT_DEFINITION_CONTEXT('',#45782,'design');
#45646=PRODUCT_DEFINITION_FORMATION_WITH_SPECIFIED_SOURCE('','',#45702,
 .NOT_KNOWN.);
#45702=PRODUCT('spring','spring','spring',(#45758));
#45758=PRODUCT_CONTEXT('',#45782,'mechanical');
#45782=APPLICATION_CONTEXT('managed model based 3d engineering');
ENDSEC;
END-ISO-10303-21;
